ISO-10303-21;
HEADER;
FILE_DESCRIPTION (('STEP AP214'),
    '1' );
FILE_NAME ('torque nut 04-2_iso_ISO 7043-M5-N.step',
    '2026-09-24T10:26:00',
    ( '' ),
    ( '' ),
    'SwSTEP 2.0',
    'SolidWorks 2026',
    '' );
FILE_SCHEMA (( 'AUTOMOTIVE_DESIGN' ));
ENDSEC;

DATA;
#9=CARTESIAN_POINT ( 'NONE',  ( -4.101948962585905356, 2.368261337751086604, -3.381124513963614575 ) ) ;
#23=ORIENTED_EDGE ( 'NONE', *, *, #4123, .F. ) ;
#27=CONICAL_SURFACE ( 'NONE', #253, 2.540000000000002700, 0.7853981633974502774 ) ;
#41=CARTESIAN_POINT ( 'NONE',  ( -2.682243648011666259, -3.070208061305319536, -0.04852650426602220929 ) ) ;
#57=DIRECTION ( 'NONE',  ( 0.000000000000000000, 0.000000000000000000, -1.000000000000000000 ) ) ;
#60=ORIENTED_EDGE ( 'NONE', *, *, #8052, .T. ) ;
#65=CARTESIAN_POINT ( 'NONE',  ( 0.000000000000000000, 0.000000000000000000, -3.699999999999981082 ) ) ;
#67=B_SPLINE_CURVE_WITH_KNOTS ( 'NONE', 3,
 ( #11560, #3741, #1534, #5910, #10391, #8105 ),
 .UNSPECIFIED., .F., .F.,
 ( 4, 2, 4 ),
 ( 0.002365888236227980772, 0.003551327329835084114, 0.004736766423442187457 ),
 .UNSPECIFIED. ) ;
#77=AXIS2_PLACEMENT_3D ( 'NONE', #6500, #5341, #2338 ) ;
#78=ORIENTED_EDGE ( 'NONE', *, *, #9945, .T. ) ;
#85=CARTESIAN_POINT ( 'NONE',  ( 2.855764796983339515, -2.970025579236438951, -0.09382832055446838071 ) ) ;
#93=AXIS2_PLACEMENT_3D ( 'NONE', #10441, #13974, #10675 ) ;
#94=CARTESIAN_POINT ( 'NONE',  ( -2.000000000000003997, 3.464101615137761492, -2.842992957459211212 ) ) ;
#103=CARTESIAN_POINT ( 'NONE',  ( 0.000000000000000000, 0.000000000000000000, 1.599999999999990319 ) ) ;
#129=FACE_OUTER_BOUND ( 'NONE', #6696, .T. ) ;
#135=ADVANCED_FACE ( 'NONE', ( #12436 ), #6529, .F. ) ;
#145=CARTESIAN_POINT ( 'NONE',  ( -2.712778981739159878, 3.052578478157618846, -3.130620751972420734 ) ) ;
#151=CARTESIAN_POINT ( 'NONE',  ( 2.171643655288374664, -3.365003104552342972, -1.643201566025979943E-14 ) ) ;
#153=FACE_OUTER_BOUND ( 'NONE', #11102, .T. ) ;
#167=CARTESIAN_POINT ( 'NONE',  ( 0.000000000000000000, 0.000000000000000000, 0.000000000000000000 ) ) ;
#194=EDGE_CURVE ( 'NONE', #2847, #8895, #12600, .T. ) ;
#203=CARTESIAN_POINT ( 'NONE',  ( -4.204114099329524734, 1.660341531092956124, -3.302132361967865748 ) ) ;
#213=EDGE_CURVE ( 'NONE', #6553, #4911, #14362, .T. ) ;
#220=EDGE_LOOP ( 'NONE', ( #2917, #1884 ) ) ;
#233=ORIENTED_EDGE ( 'NONE', *, *, #8707, .F. ) ;
#241=EDGE_CURVE ( 'NONE', #3192, #10542, #6150, .T. ) ;
#242=CARTESIAN_POINT ( 'NONE',  ( 4.000000000000003553, 2.309401076758501592, -4.699999999999981526 ) ) ;
#253=AXIS2_PLACEMENT_3D ( 'NONE', #8429, #2964, #14156 ) ;
#263=AXIS2_PLACEMENT_3D ( 'NONE', #12477, #3770, #2452 ) ;
#276=DIRECTION ( 'NONE',  ( 0.000000000000000000, 0.000000000000000000, 1.000000000000000000 ) ) ;
#295=DIRECTION ( 'NONE',  ( -1.000000000000000000, -1.665334536937734318E-16, 0.000000000000000000 ) ) ;
#299=EDGE_CURVE ( 'NONE', #11445, #8749, #1752, .T. ) ;
#315=AXIS2_PLACEMENT_3D ( 'NONE', #13880, #3856, #13947 ) ;
#317=ORIENTED_EDGE ( 'NONE', *, *, #8785, .T. ) ;
#321=CARTESIAN_POINT ( 'NONE',  ( -1.655952806101420816, 3.662737355149043417, -7.859618717572649691E-15 ) ) ;
#330=FACE_OUTER_BOUND ( 'NONE', #10664, .T. ) ;
#340=EDGE_LOOP ( 'NONE', ( #2490, #1652, #2077 ) ) ;
#342=CYLINDRICAL_SURFACE ( 'NONE', #2622, 4.000000000000001776 ) ;
#360=AXIS2_PLACEMENT_3D ( 'NONE', #1411, #10345, #9164 ) ;
#382=EDGE_CURVE ( 'NONE', #1594, #11544, #7791, .T. ) ;
#387=ORIENTED_EDGE ( 'NONE', *, *, #10769, .T. ) ;
#391=DIRECTION ( 'NONE',  ( 0.000000000000000000, -0.000000000000000000, 1.000000000000000000 ) ) ;
#396=AXIS2_PLACEMENT_3D ( 'NONE', #2897, #625, #12994 ) ;
#422=B_SPLINE_CURVE_WITH_KNOTS ( 'NONE', 3,
 ( #9433, #5309, #10938, #9845, #3882, #8317, #12794, #9770 ),
 .UNSPECIFIED., .F., .F.,
 ( 4, 2, 2, 4 ),
 ( 0.005725059856848621793, 0.006314084072593604928, 0.006903108288338587195, 0.008081156719828553464 ),
 .UNSPECIFIED. ) ;
#424=CARTESIAN_POINT ( 'NONE',  ( -4.197312189423704432, -0.8182410726374524934, -3.202520316362464481 ) ) ;
#467=CARTESIAN_POINT ( 'NONE',  ( -2.805705207896070252, 3.226868319750162861, -3.203898532754350104 ) ) ;
#478=CARTESIAN_POINT ( 'NONE',  ( 5.384454397937120440, 8.966917871450958727E-16, -4.184454397937131809 ) ) ;
#493=CARTESIAN_POINT ( 'NONE',  ( 2.000000000000015543, 3.464101615137753942, 0.000000000000000000 ) ) ;
#496=SURFACE_STYLE_USAGE ( .BOTH. , #6408 ) ;
#502=DIRECTION ( 'NONE',  ( -0.000000000000000000, -0.000000000000000000, -1.000000000000000000 ) ) ;
#526=DIRECTION ( 'NONE',  ( 1.000000000000000000, 1.665334536937734318E-16, 0.000000000000000000 ) ) ;
#555=ORIENTED_EDGE ( 'NONE', *, *, #8079, .T. ) ;
#585=ORIENTED_EDGE ( 'NONE', *, *, #12122, .F. ) ;
#592=B_SPLINE_CURVE_WITH_KNOTS ( 'NONE', 3,
 ( #1588, #2278, #11199, #5965, #2620, #12712 ),
 .UNSPECIFIED., .F., .F.,
 ( 4, 2, 4 ),
 ( -3.640115492423102241E-06, 0.0002066546034006423217, 0.0004169493222937077355 ),
 .UNSPECIFIED. ) ;
#621=UNCERTAINTY_MEASURE_WITH_UNIT (LENGTH_MEASURE( 1.000000000000000082E-05 ), #3972, 'distance_accuracy_value', 'NONE');
#622=ADVANCED_FACE ( 'NONE', ( #129 ), #8970, .F. ) ;
#623=FACE_OUTER_BOUND ( 'NONE', #7220, .T. ) ;
#625=DIRECTION ( 'NONE',  ( 0.000000000000000000, 0.000000000000000000, 1.000000000000000000 ) ) ;
#639=CARTESIAN_POINT ( 'NONE',  ( -4.000000000000000000, -2.309401076758511806, -3.133295621305376422 ) ) ;
#645=APPLICATION_CONTEXT ( 'automotive_design' ) ;
#657=ORIENTED_EDGE ( 'NONE', *, *, #4198, .F. ) ;
#661=VERTEX_POINT ( 'NONE', #10362 ) ;
#664=DIRECTION ( 'NONE',  ( -1.000000000000000000, -1.665334536937734071E-16, 0.000000000000000000 ) ) ;
#682=DIRECTION ( 'NONE',  ( 0.000000000000000000, 0.000000000000000000, 1.000000000000000000 ) ) ;
#698=VERTEX_POINT ( 'NONE', #3713 ) ;
#720=VECTOR ( 'NONE', #4602, 1000.000000000000000 ) ;
#723=ORIENTED_EDGE ( 'NONE', *, *, #10769, .F. ) ;
#738=CARTESIAN_POINT ( 'NONE',  ( 0.000000000000000000, 0.000000000000000000, -4.394516984716101859 ) ) ;
#740=AXIS2_PLACEMENT_3D ( 'NONE', #6657, #8927, #12156 ) ;
#746=LINE ( 'NONE', #10695, #6564 ) ;
#802=CARTESIAN_POINT ( 'NONE',  ( 4.000000000000003553, 2.309401076758501592, -3.133295621305376422 ) ) ;
#820=EDGE_CURVE ( 'NONE', #1356, #9307, #11728, .T. ) ;
#834=EDGE_CURVE ( 'NONE', #7523, #7727, #8404, .T. ) ;
#863=CARTESIAN_POINT ( 'NONE',  ( 4.101954839143059139, -2.368264730582945177, -3.381130640444254709 ) ) ;
#866=VECTOR ( 'NONE', #8381, 999.9999999999998863 ) ;
#891=CONICAL_SURFACE ( 'NONE', #7430, 5.560781378645576645, 1.221730476396047926 ) ;
#893=CARTESIAN_POINT ( 'NONE',  ( 3.333333333333336146, 2.694301256218253116, -3.000726591567075552 ) ) ;
#897=CARTESIAN_POINT ( 'NONE',  ( 3.436326524993614129, -2.634838109287991781, -3.231543764078655290 ) ) ;
#924=ORIENTED_EDGE ( 'NONE', *, *, #13227, .T. ) ;
#948=CARTESIAN_POINT ( 'NONE',  ( 2.000000000000000000, -3.464101615137768153, -2.842992957459220094 ) ) ;
#961=DIRECTION ( 'NONE',  ( -1.000000000000000000, -1.665334536937734071E-16, 0.000000000000000000 ) ) ;
#969=DIRECTION ( 'NONE',  ( 0.000000000000000000, 0.000000000000000000, -1.000000000000000000 ) ) ;
#982=CARTESIAN_POINT ( 'NONE',  ( 0.000000000000000000, -4.862606272033103139, -3.445885042887453231 ) ) ;
#986=ADVANCED_FACE ( 'NONE', ( #6609 ), #6751, .F. ) ;
#987=EDGE_CURVE ( 'NONE', #11970, #3878, #9444, .T. ) ;
#988=CARTESIAN_POINT ( 'NONE',  ( -2.500000000000002220, -1.101719344475953146E-16, -25.03750572909319061 ) ) ;
#991=AXIS2_PLACEMENT_3D ( 'NONE', #13701, #13850, #10320 ) ;
#1012=CARTESIAN_POINT ( 'NONE',  ( 4.154306624731433750, -2.398490048084421122, -3.421999068284433676 ) ) ;
#1021=ADVANCED_FACE ( 'NONE', ( #9987, #11652 ), #1711, .F. ) ;
#1031=DIRECTION ( 'NONE',  ( -0.5000000000000008882, 0.8660254037844381525, 0.000000000000000000 ) ) ;
#1033=AXIS2_PLACEMENT_3D ( 'NONE', #242, #7849, #9161 ) ;
#1082=CARTESIAN_POINT ( 'NONE',  ( 4.197478771013681609, -0.8523759490158168139, -3.205061274276545635 ) ) ;
#1093=CIRCLE ( 'NONE', #396, 4.000000000000000000 ) ;
#1110=AXIS2_PLACEMENT_3D ( 'NONE', #10576, #2832, #1800 ) ;
#1117=EDGE_CURVE ( 'NONE', #12838, #11202, #2635, .T. ) ;
#1136=ADVANCED_FACE ( 'NONE', ( #2736, #623 ), #7033, .F. ) ;
#1141=ORIENTED_EDGE ( 'NONE', *, *, #987, .F. ) ;
#1152=EDGE_CURVE ( 'NONE', #12756, #1916, #9781, .T. ) ;
#1156=CARTESIAN_POINT ( 'NONE',  ( 4.000000000000007105, -2.309401076758509141, -3.204271511726779043 ) ) ;
#1162=CARTESIAN_POINT ( 'NONE',  ( 4.000000000000005329, -1.560351142792950174, -0.2242961665059858556 ) ) ;
#1171=VECTOR ( 'NONE', #2786, 1000.000000000000000 ) ;
#1174=EDGE_CURVE ( 'NONE', #13588, #6553, #10290, .T. ) ;
#1175=CARTESIAN_POINT ( 'NONE',  ( -4.024497503033517276, 2.323544716729386117, -3.272167766733376393 ) ) ;
#1184=FACE_OUTER_BOUND ( 'NONE', #3982, .T. ) ;
#1222=CARTESIAN_POINT ( 'NONE',  ( -3.000000000000001332, -1.322063213371143331E-16, 13.31572692736082786 ) ) ;
#1237=CARTESIAN_POINT ( 'NONE',  ( 0.02448804030508137594, 4.877043185438126649, -3.451162025751973950 ) ) ;
#1265=CARTESIAN_POINT ( 'NONE',  ( -4.203833317240883716, -1.627343821129585422, -3.297273115243907426 ) ) ;
#1271=ADVANCED_FACE ( 'NONE', ( #7464 ), #27, .F. ) ;
#1284=ORIENTED_EDGE ( 'NONE', *, *, #12682, .T. ) ;
#1302=CARTESIAN_POINT ( 'NONE',  ( 4.197393957002307552, 0.8151795401431386479, -3.203767560748919774 ) ) ;
#1316=( BOUNDED_SURFACE ( )  B_SPLINE_SURFACE ( 3, 2, ( 
 ( #6322, #13004, #1867 ),
 ( #2909, #7475, #3125 ),
 ( #14171, #3052, #6451 ),
 ( #10861, #10721, #12039 ),
 ( #10924, #897, #3998 ),
 ( #5367, #8736, #13216 ) ),
 .UNSPECIFIED., .F., .F., .F. ) 
 B_SPLINE_SURFACE_WITH_KNOTS ( ( 4, 2, 4 ),
 ( 3, 3 ),
 ( 0.02023740217035201183, 0.02269762987400600340, 0.02515785757765999150 ),
 ( 0.000000000000000000, 1.000000000000000000 ),
 .UNSPECIFIED. ) 
 GEOMETRIC_REPRESENTATION_ITEM ( )  RATIONAL_B_SPLINE_SURFACE ( (
 ( 1.000000000000000000, 0.8047781539129729156, 1.000000000000000000),
 ( 1.000000000000000000, 0.8123770319059264722, 1.000000000000000000),
 ( 1.000000000000000000, 0.8190663783054025204, 1.000000000000000000),
 ( 1.000000000000000000, 0.8192359702879900007, 1.000000000000000000),
 ( 1.000000000000000000, 0.8126134888417688718, 1.000000000000000000),
 ( 1.000000000000000000, 0.8047712368238112424, 1.000000000000000000) ) ) 
 REPRESENTATION_ITEM ( '' )  SURFACE ( )  );
#1356=VERTEX_POINT ( 'NONE', #1506 ) ;
#1357=PLANE ( 'NONE',  #13573 ) ;
#1369=CARTESIAN_POINT ( 'NONE',  ( -0.6641139335926458109, 4.471067008845417412, -3.302142222888703849 ) ) ;
#1390=CARTESIAN_POINT ( 'NONE',  ( -2.171643655288370667, 3.365003104552331870, -7.639672495602285140E-15 ) ) ;
#1404=EDGE_CURVE ( 'NONE', #6344, #11164, #11446, .T. ) ;
#1411=CARTESIAN_POINT ( 'NONE',  ( 0.000000000000000000, 0.000000000000000000, 0.000000000000000000 ) ) ;
#1412=CARTESIAN_POINT ( 'NONE',  ( 0.000000000000000000, 0.000000000000000000, -4.674599999999973221 ) ) ;
#1466=AXIS2_PLACEMENT_3D ( 'NONE', #11474, #5689, #295 ) ;
#1479=ORIENTED_EDGE ( 'NONE', *, *, #1749, .F. ) ;
#1499=ADVANCED_FACE ( 'NONE', ( #1184 ), #8661, .T. ) ;
#1501=CARTESIAN_POINT ( 'NONE',  ( 1.390214784104953027, 4.043996922316329901, -3.202509183706280460 ) ) ;
#1506=CARTESIAN_POINT ( 'NONE',  ( 0.000000000000000000, -4.862606272033103139, -3.445885042887453231 ) ) ;
#1524=CARTESIAN_POINT ( 'NONE',  ( 4.101954839143062692, 2.368264730582934519, -3.381130640444258262 ) ) ;
#1529=DIRECTION ( 'NONE',  ( 1.000000000000000000, 1.665334536937734071E-16, 0.000000000000000000 ) ) ;
#1534=CARTESIAN_POINT ( 'NONE',  ( 1.317756351988342622, -3.857995168970220767, -0.04852650426603082046 ) ) ;
#1540=ORIENTED_EDGE ( 'NONE', *, *, #4596, .F. ) ;
#1543=ADVANCED_FACE ( 'NONE', ( #11133 ), #11023, .F. ) ;
#1548=DIRECTION ( 'NONE',  ( 0.000000000000000000, 0.000000000000000000, 1.000000000000000000 ) ) ;
#1566=CARTESIAN_POINT ( 'NONE',  ( 3.472352378023054520, 2.614038573344155125, -3.020318136128903319 ) ) ;
#1578=CARTESIAN_POINT ( 'NONE',  ( 3.679171394226034231, 2.494631558665835858, -0.3503314178412536006 ) ) ;
#1588=CARTESIAN_POINT ( 'NONE',  ( 0.000000000000000000, 4.862606272033096033, -3.445885042887453231 ) ) ;
#1591=CARTESIAN_POINT ( 'NONE',  ( 4.024499207728662320, 2.323545700935577329, -3.272172305156505701 ) ) ;
#1594=VERTEX_POINT ( 'NONE', #6951 ) ;
#1619=VECTOR ( 'NONE', #9205, 1000.000000000000000 ) ;
#1620=LINE ( 'NONE', #14009, #6263 ) ;
#1630=DIRECTION ( 'NONE',  ( 1.000000000000000000, 1.665334536937734071E-16, 0.000000000000000000 ) ) ;
#1650=ORIENTED_EDGE ( 'NONE', *, *, #2508, .F. ) ;
#1652=ORIENTED_EDGE ( 'NONE', *, *, #12936, .T. ) ;
#1660=AXIS2_PLACEMENT_3D ( 'NONE', #13162, #6050, #12116 ) ;
#1662=ORIENTED_EDGE ( 'NONE', *, *, #820, .T. ) ;
#1692=CARTESIAN_POINT ( 'NONE',  ( 0.000000000000000000, 0.000000000000000000, 13.31572692736082786 ) ) ;
#1698=CARTESIAN_POINT ( 'NONE',  ( -4.024497503033519052, -2.323544716729397219, -3.272167766733379946 ) ) ;
#1707=DIRECTION ( 'NONE',  ( 1.000000000000000000, 1.665334536937733825E-16, 0.000000000000000000 ) ) ;
#1711=PLANE ( 'NONE',  #10377 ) ;
#1729=LINE ( 'NONE', #7412, #13044 ) ;
#1731=CARTESIAN_POINT ( 'NONE',  ( -4.000000000000000888, -1.539600717839011423, -3.000726591567076884 ) ) ;
#1749=EDGE_CURVE ( 'NONE', #6344, #12541, #746, .T. ) ;
#1750=CARTESIAN_POINT ( 'NONE',  ( 1.144235203016672475, 3.958177651039092471, -0.09382832055445862462 ) ) ;
#1752=LINE ( 'NONE', #6125, #2421 ) ;
#1762=CARTESIAN_POINT ( 'NONE',  ( -4.204015924366186319, 1.626724848190924000, -3.310627190413372389 ) ) ;
#1775=EDGE_CURVE ( 'NONE', #9307, #7122, #7738, .T. ) ;
#1792=ORIENTED_EDGE ( 'NONE', *, *, #12682, .F. ) ;
#1797=DIRECTION ( 'NONE',  ( 1.665334536937734071E-16, -1.000000000000000000, 0.000000000000000000 ) ) ;
#1800=DIRECTION ( 'NONE',  ( 1.000000000000000000, 1.665334536937734071E-16, 0.000000000000000000 ) ) ;
#1803=EDGE_LOOP ( 'NONE', ( #8409, #10422, #4006 ) ) ;
#1817=CARTESIAN_POINT ( 'NONE',  ( 1.654252653721915101, 3.663718938583012008, -0.01223254789873715748 ) ) ;
#1820=ORIENTED_EDGE ( 'NONE', *, *, #1404, .T. ) ;
#1827=B_SPLINE_CURVE_WITH_KNOTS ( 'NONE', 3,
 ( #12263, #8814, #41, #8955, #3271, #5521 ),
 .UNSPECIFIED., .F., .F.,
 ( 4, 2, 4 ),
 ( 0.002365888236227998986, 0.003551327329835089319, 0.004736766423442179651 ),
 .UNSPECIFIED. ) ;
#1867=CARTESIAN_POINT ( 'NONE',  ( -0.02448804030508153901, -4.877043185438141748, -3.451162025751979279 ) ) ;
#1884=ORIENTED_EDGE ( 'NONE', *, *, #13910, .F. ) ;
#1900=FACE_OUTER_BOUND ( 'NONE', #3304, .T. ) ;
#1910=ORIENTED_EDGE ( 'NONE', *, *, #12743, .F. ) ;
#1916=VERTEX_POINT ( 'NONE', #3385 ) ;
#1924=AXIS2_PLACEMENT_3D ( 'NONE', #7914, #10455, #3739 ) ;
#1927=FACE_OUTER_BOUND ( 'NONE', #1803, .T. ) ;
#1939=CARTESIAN_POINT ( 'NONE',  ( 2.540000000000002700, 4.229949723821848943E-16, 1.599999999999990319 ) ) ;
#1940=ORIENTED_EDGE ( 'NONE', *, *, #8566, .F. ) ;
#1945=FACE_OUTER_BOUND ( 'NONE', #3904, .T. ) ;
#1947=DIRECTION ( 'NONE',  ( 1.000000000000000000, 1.665334536937734564E-16, 0.000000000000000000 ) ) ;
#1966=CARTESIAN_POINT ( 'NONE',  ( 2.000000000000015543, 3.464101615137753942, 0.000000000000000000 ) ) ;
#1992=EDGE_CURVE ( 'NONE', #8895, #4249, #13765, .T. ) ;
#2010=DIRECTION ( 'NONE',  ( -0.5000000000000014433, -0.8660254037844378194, 0.000000000000000000 ) ) ;
#2013=DIRECTION ( 'NONE',  ( 0.8191520442889900222, 2.367334119411125886E-16, -0.5735764363510484909 ) ) ;
#2059=DIRECTION ( 'NONE',  ( -1.000000000000000000, -1.665334536937734071E-16, 0.000000000000000000 ) ) ;
#2077=ORIENTED_EDGE ( 'NONE', *, *, #5682, .F. ) ;
#2083=CIRCLE ( 'NONE', #6471, 0.5155456020628804703 ) ;
#2097=AXIS2_PLACEMENT_3D ( 'NONE', #65, #12421, #13311 ) ;
#2126=DIRECTION ( 'NONE',  ( 0.000000000000000000, 0.000000000000000000, 1.000000000000000000 ) ) ;
#2133=CARTESIAN_POINT ( 'NONE',  ( 3.333333333333336146, -2.694301256218264662, -3.000726591567077328 ) ) ;
#2135=CIRCLE ( 'NONE', #1660, 2.540000000000002700 ) ;
#2137=DIRECTION ( 'NONE',  ( 1.000000000000000000, 1.665334536937734318E-16, 0.000000000000000000 ) ) ;
#2156=EDGE_LOOP ( 'NONE', ( #924, #6342 ) ) ;
#2159=ORIENTED_EDGE ( 'NONE', *, *, #10171, .T. ) ;
#2181=B_SPLINE_CURVE_WITH_KNOTS ( 'NONE', 3,
 ( #2717, #11627, #5267, #1762, #5192, #7382 ),
 .UNSPECIFIED., .F., .F.,
 ( 4, 2, 4 ),
 ( 0.002452478801916370670, 0.003676905084148003947, 0.004901331366379637657 ),
 .UNSPECIFIED. ) ;
#2187=EDGE_CURVE ( 'NONE', #2424, #6911, #12850, .T. ) ;
#2197=CONICAL_SURFACE ( 'NONE', #4080, 4.000000000000000000, 0.8911886515913775009 ) ;
#2204=ORIENTED_EDGE ( 'NONE', *, *, #8603, .T. ) ;
#2210=ORIENTED_EDGE ( 'NONE', *, *, #4596, .T. ) ;
#2215=CARTESIAN_POINT ( 'NONE',  ( -3.999999999999996447, 2.309401076758494487, -3.133295621305376422 ) ) ;
#2216=VERTEX_POINT ( 'NONE', #3151 ) ;
#2242=CARTESIAN_POINT ( 'NONE',  ( 4.000000000000003553, -2.309401076758511806, -0.5000000000000004441 ) ) ;
#2262=CARTESIAN_POINT ( 'NONE',  ( 4.197310878070203088, 0.8178547585014672716, -3.202500312981924502 ) ) ;
#2269=CARTESIAN_POINT ( 'NONE',  ( -1.257202807339061090, 3.892955774274172054, -3.133250573521038085 ) ) ;
#2276=CARTESIAN_POINT ( 'NONE',  ( -4.154094228333303107, 2.398367420968265495, -3.421909803043239329 ) ) ;
#2278=CARTESIAN_POINT ( 'NONE',  ( -3.549493361947295804E-13, 4.796734841935104576, -3.421909803043237552 ) ) ;
#2282=VECTOR ( 'NONE', #2013, 1000.000000000000114 ) ;
#2296=CYLINDRICAL_SURFACE ( 'NONE', #3123, 4.000000000000001776 ) ;
#2298=AXIS2_PLACEMENT_3D ( 'NONE', #3726, #502, #4960 ) ;
#2300=AXIS2_PLACEMENT_3D ( 'NONE', #4455, #4652, #9995 ) ;
#2315=ORIENTED_EDGE ( 'NONE', *, *, #8603, .F. ) ;
#2338=DIRECTION ( 'NONE',  ( 1.000000000000000000, 1.665334536937734318E-16, 0.000000000000000000 ) ) ;
#2347=ORIENTED_EDGE ( 'NONE', *, *, #194, .T. ) ;
#2353=ORIENTED_EDGE ( 'NONE', *, *, #6759, .T. ) ;
#2366=CARTESIAN_POINT ( 'NONE',  ( -4.197393957002300446, -0.8151795401431400911, -3.203767560748917553 ) ) ;
#2384=CARTESIAN_POINT ( 'NONE',  ( -3.999999999999996447, -1.560351142792946399, -0.2242961665059788057 ) ) ;
#2395=AXIS2_PLACEMENT_3D ( 'NONE', #1692, #11792, #526 ) ;
#2401=CARTESIAN_POINT ( 'NONE',  ( 2.500000000000002220, 4.163336342344338999E-16, -4.699999999999981526 ) ) ;
#2402=DIRECTION ( 'NONE',  ( 0.000000000000000000, 0.000000000000000000, 1.000000000000000000 ) ) ;
#2406=AXIS2_PLACEMENT_3D ( 'NONE', #13405, #9944, #14349 ) ;
#2407=ORIENTED_EDGE ( 'NONE', *, *, #820, .F. ) ;
#2408=CARTESIAN_POINT ( 'NONE',  ( -4.141042022537586575, 2.227970427079376314, -3.387027626239150546 ) ) ;
#2421=VECTOR ( 'NONE', #11545, 1000.000000000000000 ) ;
#2422=DIRECTION ( 'NONE',  ( 0.000000000000000000, 0.000000000000000000, 1.000000000000000000 ) ) ;
#2424=VERTEX_POINT ( 'NONE', #6774 ) ;
#2431=EDGE_CURVE ( 'NONE', #2216, #6532, #8082, .T. ) ;
#2434=DIRECTION ( 'NONE',  ( -0.9396926207859144231, -1.564902575500316617E-16, -0.3420201433256524481 ) ) ;
#2439=ORIENTED_EDGE ( 'NONE', *, *, #5332, .T. ) ;
#2452=DIRECTION ( 'NONE',  ( 1.000000000000000000, 1.665334536937734318E-16, 0.000000000000000000 ) ) ;
#2472=CARTESIAN_POINT ( 'NONE',  ( -4.197477404309741367, 0.8522071663317644097, -3.205040426610007209 ) ) ;
#2490=ORIENTED_EDGE ( 'NONE', *, *, #13049, .F. ) ;
#2508=EDGE_CURVE ( 'NONE', #7523, #2748, #8301, .T. ) ;
#2552=CARTESIAN_POINT ( 'NONE',  ( 0.1750032273043234943, 4.719840313910212082, -3.169254239516200222 ) ) ;
#2554=VERTEX_POINT ( 'NONE', #2924 ) ;
#2555=CARTESIAN_POINT ( 'NONE',  ( 0.000000000000000000, 4.618802153517016507, -4.699999999999981526 ) ) ;
#2576=( NAMED_UNIT ( * ) SI_UNIT ( $, .STERADIAN. ) SOLID_ANGLE_UNIT ( ) );
#2582=DIRECTION ( 'NONE',  ( 0.000000000000000000, 0.000000000000000000, 1.000000000000000000 ) ) ;
#2608=CARTESIAN_POINT ( 'NONE',  ( 0.000000000000000000, 0.000000000000000000, 13.31572692736082786 ) ) ;
#2620=CARTESIAN_POINT ( 'NONE',  ( 4.814824860968092917E-32, 4.618802153517016507, -3.204269196027521360 ) ) ;
#2622=AXIS2_PLACEMENT_3D ( 'NONE', #2608, #10427, #13957 ) ;
#2623=EDGE_CURVE ( 'NONE', #1594, #11164, #8747, .T. ) ;
#2626=CIRCLE ( 'NONE', #10812, 2.100000000000000977 ) ;
#2630=ORIENTED_EDGE ( 'NONE', *, *, #8123, .T. ) ;
#2635=B_SPLINE_CURVE_WITH_KNOTS ( 'NONE', 3,
 ( #10342, #321, #12750, #4782, #8129, #8207 ),
 .UNSPECIFIED., .F., .F.,
 ( 4, 2, 4 ),
 ( 0.002365888236227976869, 0.003551327329835078477, 0.004736766423442180518 ),
 .UNSPECIFIED. ) ;
#2641=AXIS2_PLACEMENT_3D ( 'NONE', #3840, #11649, #1707 ) ;
#2678=ORIENTED_EDGE ( 'NONE', *, *, #8571, .T. ) ;
#2698=CARTESIAN_POINT ( 'NONE',  ( -3.999999999999992006, 0.8576023918602521112, -3.133238574225018613 ) ) ;
#2708=CARTESIAN_POINT ( 'NONE',  ( -1.654252653721914434, -3.663718938583019558, -0.01223254789874345973 ) ) ;
#2712=DIRECTION ( 'NONE',  ( 0.000000000000000000, 0.000000000000000000, 1.000000000000000000 ) ) ;
#2717=CARTESIAN_POINT ( 'NONE',  ( -4.197393957002300446, -7.772664289393031077E-14, -3.203767560748911780 ) ) ;
#2736=FACE_BOUND ( 'NONE', #13542, .T. ) ;
#2745=EDGE_CURVE ( 'NONE', #2216, #1356, #3906, .T. ) ;
#2748=VERTEX_POINT ( 'NONE', #5786 ) ;
#2753=CARTESIAN_POINT ( 'NONE',  ( 4.235887314095731604, 2.417314327725962997, -3.451162025751971729 ) ) ;
#2777=FACE_OUTER_BOUND ( 'NONE', #11779, .T. ) ;
#2781=CARTESIAN_POINT ( 'NONE',  ( 4.000000000000003553, 2.309401076758501592, -3.133295621305376422 ) ) ;
#2786=DIRECTION ( 'NONE',  ( 0.000000000000000000, 0.000000000000000000, 1.000000000000000000 ) ) ;
#2796=CARTESIAN_POINT ( 'NONE',  ( -3.999999999999996447, -2.309401076758511806, -0.5000000000000004441 ) ) ;
#2809=CARTESIAN_POINT ( 'NONE',  ( 4.000000000000003553, 0.9868501483902586413, -0.09357334158579964922 ) ) ;
#2830=FACE_OUTER_BOUND ( 'NONE', #3497, .T. ) ;
#2832=DIRECTION ( 'NONE',  ( 0.000000000000000000, 0.000000000000000000, 1.000000000000000000 ) ) ;
#2834=CARTESIAN_POINT ( 'NONE',  ( -2.500000000000002220, -4.163336342344338999E-16, -4.674599999999973221 ) ) ;
#2847=VERTEX_POINT ( 'NONE', #2242 ) ;
#2869=CARTESIAN_POINT ( 'NONE',  ( 3.510273485745313948, 2.827716139362655756, -3.310536846335870642 ) ) ;
#2882=CIRCLE ( 'NONE', #991, 3.200000000000000622 ) ;
#2885=B_SPLINE_CURVE_WITH_KNOTS ( 'NONE', 3,
 ( #6282, #12972, #8257, #12884, #10755, #2869, #6354, #9440 ),
 .UNSPECIFIED., .F., .F.,
 ( 4, 2, 2, 4 ),
 ( 5.712950814681226391E-18, 0.002450665683189820563, 0.003675998524784728026, 0.004901331366379636789 ),
 .UNSPECIFIED. ) ;
#2897=CARTESIAN_POINT ( 'NONE',  ( 0.000000000000000000, 0.000000000000000000, 0.000000000000000000 ) ) ;
#2901=ORIENTED_EDGE ( 'NONE', *, *, #4793, .F. ) ;
#2909=CARTESIAN_POINT ( 'NONE',  ( 0.5276476219768478915, -4.314164656931422925, -3.020318136128777642 ) ) ;
#2916=CARTESIAN_POINT ( 'NONE',  ( 0.000000000000000000, 0.000000000000000000, 1.599999999999990319 ) ) ;
#2917=ORIENTED_EDGE ( 'NONE', *, *, #9650, .F. ) ;
#2924=CARTESIAN_POINT ( 'NONE',  ( 2.540000000000002700, 4.229949723821848943E-16, 1.599999999999990319 ) ) ;
#2932=EDGE_CURVE ( 'NONE', #6869, #11164, #12087, .T. ) ;
#2939=DIRECTION ( 'NONE',  ( 0.000000000000000000, 0.000000000000000000, -1.000000000000000000 ) ) ;
#2964=DIRECTION ( 'NONE',  ( 0.000000000000000000, 0.000000000000000000, 1.000000000000000000 ) ) ;
#2984=ORIENTED_EDGE ( 'NONE', *, *, #1152, .F. ) ;
#3015=CIRCLE ( 'NONE', #12342, 4.000000000000000000 ) ;
#3036=CARTESIAN_POINT ( 'NONE',  ( 4.000000000000004441, 1.563622288139198568, -0.2253451193528359653 ) ) ;
#3052=CARTESIAN_POINT ( 'NONE',  ( 1.257202807339443673, -3.892955774273464620, -3.133250573521783267 ) ) ;
#3084=PLANE ( 'NONE',  #4411 ) ;
#3088=CARTESIAN_POINT ( 'NONE',  ( 3.999999999999998224, 1.680235903636351003, -3.016633206402824730 ) ) ;
#3113=PLANE ( 'NONE',  #5740 ) ;
#3123=AXIS2_PLACEMENT_3D ( 'NONE', #9081, #6607, #3411 ) ;
#3124=EDGE_CURVE ( 'NONE', #14315, #2424, #1093, .T. ) ;
#3125=CARTESIAN_POINT ( 'NONE',  ( 0.6641139335914896247, -4.471067008845462709, -3.302142222888722500 ) ) ;
#3138=CARTESIAN_POINT ( 'NONE',  ( -0.3198814748697705879, -4.434118497892186817, -0.3507732604232561280 ) ) ;
#3145=CARTESIAN_POINT ( 'NONE',  ( 0.000000000000000000, 0.000000000000000000, 13.31572692736082786 ) ) ;
#3149=ORIENTED_EDGE ( 'NONE', *, *, #9166, .T. ) ;
#3151=CARTESIAN_POINT ( 'NONE',  ( 0.000000000000000000, -4.618802153517030717, -3.133295621305376422 ) ) ;
#3156=CARTESIAN_POINT ( 'NONE',  ( 3.999999999999998224, -0.8732118962410245766, -2.923153487222556191 ) ) ;
#3176=CARTESIAN_POINT ( 'NONE',  ( -3.472352378023202846, -2.614038573344081406, -3.020318136128327335 ) ) ;
#3192=VERTEX_POINT ( 'NONE', #14017 ) ;
#3195=CARTESIAN_POINT ( 'NONE',  ( 4.207491450040564906, -2.029819825146478074, -3.371670828759588012 ) ) ;
#3220=CARTESIAN_POINT ( 'NONE',  ( 3.999999999999999112, -2.511476383524243072, -3.169254053377029923 ) ) ;
#3234=ORIENTED_EDGE ( 'NONE', *, *, #8785, .F. ) ;
#3237=SHAPE_REPRESENTATION_RELATIONSHIP ( 'NONE' , 'NONE' ,  #8883, #13802 ) ;
#3246=CARTESIAN_POINT ( 'NONE',  ( -4.175003227304313391, -2.208362916365310902, -3.169254239516198890 ) ) ;
#3258=ORIENTED_EDGE ( 'NONE', *, *, #12743, .T. ) ;
#3271=CARTESIAN_POINT ( 'NONE',  ( -3.679171394226031122, -2.494631558665846516, -0.3503314178412552105 ) ) ;
#3273=FACE_OUTER_BOUND ( 'NONE', #7493, .T. ) ;
#3304=EDGE_LOOP ( 'NONE', ( #1284, #4695, #387, #6746, #5667 ) ) ;
#3314=CARTESIAN_POINT ( 'NONE',  ( -4.000000000000000000, 2.309401076758492266, -3.204269196027521804 ) ) ;
#3317=CARTESIAN_POINT ( 'NONE',  ( 0.000000000000000000, 0.000000000000000000, 0.000000000000000000 ) ) ;
#3325=CARTESIAN_POINT ( 'NONE',  ( -3.453019673806352774, -2.625200315326694067, -3.235259548910466076 ) ) ;
#3335=ADVANCED_FACE ( 'NONE', ( #6741 ), #3113, .T. ) ;
#3342=ORIENTED_EDGE ( 'NONE', *, *, #13049, .T. ) ;
#3353=ORIENTED_EDGE ( 'NONE', *, *, #4645, .F. ) ;
#3366=B_SPLINE_CURVE_WITH_KNOTS ( 'NONE', 3,
 ( #10630, #10844, #10906, #3978, #2809, #3036, #10775, #9676 ),
 .UNSPECIFIED., .F., .F.,
 ( 4, 2, 2, 4 ),
 ( 0.005725059856848626130, 0.006314084072593611867, 0.006903108288338597603, 0.008081156719828569077 ),
 .UNSPECIFIED. ) ;
#3374=CARTESIAN_POINT ( 'NONE',  ( 3.999999999999998224, 0.8378468363844258082, -2.920592527564365160 ) ) ;
#3378=AXIS2_PLACEMENT_3D ( 'NONE', #9933, #7578, #5467 ) ;
#3385=CARTESIAN_POINT ( 'NONE',  ( 0.000000000000000000, 4.862606272033096033, -3.445885042887453231 ) ) ;
#3389=CARTESIAN_POINT ( 'NONE',  ( -4.211140560182194292, 2.431303136016534250, -3.445885042887453231 ) ) ;
#3392=CARTESIAN_POINT ( 'NONE',  ( 0.000000000000000000, 0.000000000000000000, -4.699999999999981526 ) ) ;
#3397=CARTESIAN_POINT ( 'NONE',  ( 3.200000000000000622, 5.329070518200750211E-16, 2.400000000000013234 ) ) ;
#3411=DIRECTION ( 'NONE',  ( 1.000000000000000000, 1.665334536937734071E-16, 0.000000000000000000 ) ) ;
#3413=ORIENTED_EDGE ( 'NONE', *, *, #213, .T. ) ;
#3425=EDGE_LOOP ( 'NONE', ( #9427, #1910 ) ) ;
#3426=ORIENTED_EDGE ( 'NONE', *, *, #13922, .F. ) ;
#3444=CARTESIAN_POINT ( 'NONE',  ( -1.243833333691479526, 3.900674643483201365, -2.923144239647233356 ) ) ;
#3478=ADVANCED_FACE ( 'NONE', ( #10282 ), #342, .T. ) ;
#3497=EDGE_LOOP ( 'NONE', ( #233, #6823, #1820, #10465 ) ) ;
#3513=EDGE_CURVE ( 'NONE', #7122, #2216, #7020, .T. ) ;
#3515=CARTESIAN_POINT ( 'NONE',  ( -3.455075492487776234, 2.624013387858708413, -3.016622336521908920 ) ) ;
#3516=ORIENTED_EDGE ( 'NONE', *, *, #4793, .T. ) ;
#3535=AXIS2_PLACEMENT_3D ( 'NONE', #11507, #5932, #7175 ) ;
#3539=B_SPLINE_CURVE_WITH_KNOTS ( 'NONE', 3,
 ( #4796, #8144, #11971, #5234, #11900, #7194, #6181, #10653 ),
 .UNSPECIFIED., .F., .F.,
 ( 4, 2, 2, 4 ),
 ( 0.000000000000000000, 0.002450665683189818828, 0.003675998524784728459, 0.004901331366379637657 ),
 .UNSPECIFIED. ) ;
#3555=STYLED_ITEM ( 'NONE', ( #9810 ), #13802 ) ;
#3600=DIRECTION ( 'NONE',  ( 1.000000000000000000, 1.665334536937734318E-16, 0.000000000000000000 ) ) ;
#3615=ORIENTED_EDGE ( 'NONE', *, *, #8571, .F. ) ;
#3634=DIRECTION ( 'NONE',  ( 0.000000000000000000, 0.000000000000000000, 1.000000000000000000 ) ) ;
#3668=CARTESIAN_POINT ( 'NONE',  ( -5.560781378645534900, -2.450568166102175686E-16, -3.699999999999981082 ) ) ;
#3675=CARTESIAN_POINT ( 'NONE',  ( -2.345747346278098888, 3.264484291692505202, -0.01223254789874009263 ) ) ;
#3684=DIRECTION ( 'NONE',  ( 1.000000000000000000, 1.665334536937734071E-16, 0.000000000000000000 ) ) ;
#3713=CARTESIAN_POINT ( 'NONE',  ( -3.999999999999996447, 2.309401076758494487, -3.133295621305376422 ) ) ;
#3723=CARTESIAN_POINT ( 'NONE',  ( 2.100000000000000977, 3.497202527569243497E-16, 1.159999999999994369 ) ) ;
#3726=CARTESIAN_POINT ( 'NONE',  ( 0.000000000000000000, 0.000000000000000000, -4.699999999999981526 ) ) ;
#3730=ORIENTED_EDGE ( 'NONE', *, *, #1749, .T. ) ;
#3734=CARTESIAN_POINT ( 'NONE',  ( 4.000000000000001776, 6.661338147750939243E-16, 13.31572692736082786 ) ) ;
#3739=DIRECTION ( 'NONE',  ( 1.000000000000000000, 1.665334536937734071E-16, 0.000000000000000000 ) ) ;
#3741=CARTESIAN_POINT ( 'NONE',  ( 1.655952806101424146, -3.662737355149054963, -1.706474927185875547E-14 ) ) ;
#3755=CONICAL_SURFACE ( 'NONE', #11940, 2.540000000000002700, 0.7853981633974502774 ) ;
#3756=ORIENTED_EDGE ( 'NONE', *, *, #8491, .T. ) ;
#3761=CIRCLE ( 'NONE', #6546, 4.000000000000000000 ) ;
#3770=DIRECTION ( 'NONE',  ( 0.000000000000000000, 0.000000000000000000, 1.000000000000000000 ) ) ;
#3791=CARTESIAN_POINT ( 'NONE',  ( 2.682243648011671588, 3.070208061305306213, -0.04852650426601810146 ) ) ;
#3802=CARTESIAN_POINT ( 'NONE',  ( -3.999999999999991562, 2.511479357205549157, -3.169254599242359305 ) ) ;
#3803=CARTESIAN_POINT ( 'NONE',  ( -2.100000000000000089, -9.254442493598001840E-17, 1.159999999999994369 ) ) ;
#3822=CIRCLE ( 'NONE', #2406, 4.000000000000000000 ) ;
#3825=EDGE_LOOP ( 'NONE', ( #23, #12009, #7737, #4310 ) ) ;
#3840=CARTESIAN_POINT ( 'NONE',  ( 0.000000000000000000, 0.000000000000000000, -4.699999999999981526 ) ) ;
#3850=DIRECTION ( 'NONE',  ( 1.000000000000000000, 1.665334536937734071E-16, 0.000000000000000000 ) ) ;
#3856=DIRECTION ( 'NONE',  ( 0.000000000000000000, 0.000000000000000000, -1.000000000000000000 ) ) ;
#3857=ORIENTED_EDGE ( 'NONE', *, *, #6417, .F. ) ;
#3878=VERTEX_POINT ( 'NONE', #9388 ) ;
#3882=CARTESIAN_POINT ( 'NONE',  ( -3.999999999999996447, 0.9868501483902497595, -0.09357334158579269645 ) ) ;
#3904=EDGE_LOOP ( 'NONE', ( #12922, #13029, #8344, #1792 ) ) ;
#3906=B_SPLINE_CURVE_WITH_KNOTS ( 'NONE', 3,
 ( #11304, #6616, #13585, #8062, #5586, #7855 ),
 .UNSPECIFIED., .F., .F.,
 ( 4, 2, 4 ),
 ( 0.000000000000000000, 0.0002095117440854745035, 0.0004190234881709490071 ),
 .UNSPECIFIED. ) ;
#3934=CARTESIAN_POINT ( 'NONE',  ( -1.999999999999994005, -3.464101615137768597, -2.842992957459221426 ) ) ;
#3937=PRODUCT ( 'torque nut 04-2_iso_ISO 7043-M5-N', 'torque nut 04-2_iso_ISO 7043-M5-N', '', ( #11856 ) ) ;
#3941=CARTESIAN_POINT ( 'NONE',  ( 3.000000000000001332, 4.996003610813205418E-16, 1.599999999999990319 ) ) ;
#3956=CARTESIAN_POINT ( 'NONE',  ( -0.6448876103708461871, -4.246476118072359363, -0.2256878752776786956 ) ) ;
#3972=( LENGTH_UNIT ( ) NAMED_UNIT ( * ) SI_UNIT ( .MILLI., .METRE. ) );
#3978=CARTESIAN_POINT ( 'NONE',  ( 4.000000000000002665, 0.7924765000094613487, -0.05906175389890213484 ) ) ;
#3982=EDGE_LOOP ( 'NONE', ( #2204, #5798, #9755, #3615 ) ) ;
#3984=CARTESIAN_POINT ( 'NONE',  ( -7.999999999999992895, 0.000000000000000000, -4.699999999999981526 ) ) ;
#3998=CARTESIAN_POINT ( 'NONE',  ( 3.522881874163210636, -2.820349071480532377, -3.298443181295927840 ) ) ;
#4003=ORIENTED_EDGE ( 'NONE', *, *, #4989, .T. ) ;
#4006=ORIENTED_EDGE ( 'NONE', *, *, #4989, .F. ) ;
#4013=ORIENTED_EDGE ( 'NONE', *, *, #4873, .T. ) ;
#4017=EDGE_LOOP ( 'NONE', ( #12721, #2901, #13639 ) ) ;
#4020=COLOUR_RGB ( '', 0.31764706, 0.68627451, 0.89019608) ;
#4027=CARTESIAN_POINT ( 'NONE',  ( 4.000000000000002665, 2.309401076758501592, -3.204271511726781707 ) ) ;
#4051=ORIENTED_EDGE ( 'NONE', *, *, #10125, .F. ) ;
#4079=CARTESIAN_POINT ( 'NONE',  ( 0.000000000000000000, 0.000000000000000000, 0.000000000000000000 ) ) ;
#4080=AXIS2_PLACEMENT_3D ( 'NONE', #4206, #10845, #6158 ) ;
#4089=B_SPLINE_CURVE_WITH_KNOTS ( 'NONE', 3,
 ( #13754, #4570, #94, #4814, #9344 ),
 .UNSPECIFIED., .F., .F.,
 ( 4, 1, 4 ),
 ( 0.000000000000000000, 0.002309401076758504923, 0.004618802153517009845 ),
 .UNSPECIFIED. ) ;
#4096=CARTESIAN_POINT ( 'NONE',  ( 4.197393957002308440, -0.4069871074557449564, -3.203767560748910892 ) ) ;
#4105=( NAMED_UNIT ( * ) PLANE_ANGLE_UNIT ( ) SI_UNIT ( $, .RADIAN. ) );
#4116=CARTESIAN_POINT ( 'NONE',  ( 0.000000000000000000, 0.000000000000000000, 0.000000000000000000 ) ) ;
#4123=EDGE_CURVE ( 'NONE', #7536, #12258, #10688, .T. ) ;
#4142=ORIENTED_EDGE ( 'NONE', *, *, #12817, .F. ) ;
#4168=( NAMED_UNIT ( * ) SI_UNIT ( $, .STERADIAN. ) SOLID_ANGLE_UNIT ( ) );
#4175=ORIENTED_EDGE ( 'NONE', *, *, #9212, .F. ) ;
#4198=EDGE_CURVE ( 'NONE', #661, #12838, #9522, .T. ) ;
#4206=CARTESIAN_POINT ( 'NONE',  ( 0.000000000000000000, 0.000000000000000000, 0.000000000000000000 ) ) ;
#4213=CARTESIAN_POINT ( 'NONE',  ( 4.000000000000003553, 2.309401076758501592, -3.133295621305376422 ) ) ;
#4249=VERTEX_POINT ( 'NONE', #4908 ) ;
#4278=SURFACE_SIDE_STYLE ('',( #7672 ) ) ;
#4281=AXIS2_PLACEMENT_3D ( 'NONE', #8993, #1031, #10098 ) ;
#4287=CARTESIAN_POINT ( 'NONE',  ( -4.140405595019058360, -2.228337868678527123, -3.386887224136953201 ) ) ;
#4310=ORIENTED_EDGE ( 'NONE', *, *, #6759, .F. ) ;
#4323=AXIS2_PLACEMENT_3D ( 'NONE', #10259, #10188, #10055 ) ;
#4338=ORIENTED_EDGE ( 'NONE', *, *, #11968, .T. ) ;
#4354=CARTESIAN_POINT ( 'NONE',  ( -0.5449245075112842951, -4.304189842417356360, -3.016622336521895598 ) ) ;
#4369=LINE ( 'NONE', #9013, #5204 ) ;
#4393=AXIS2_PLACEMENT_3D ( 'NONE', #11071, #13432, #8724 ) ;
#4401=CIRCLE ( 'NONE', #1110, 4.000000000000000888 ) ;
#4411=AXIS2_PLACEMENT_3D ( 'NONE', #7583, #5401, #12211 ) ;
#4426=FACE_OUTER_BOUND ( 'NONE', #5090, .T. ) ;
#4436=TOROIDAL_SURFACE ( 'NONE', #10955, 5.384454397937117776, 0.5155456020628805813 ) ;
#4444=CARTESIAN_POINT ( 'NONE',  ( 2.500000000000002220, 7.224953340212723619E-16, -4.674599999999973221 ) ) ;
#4455=CARTESIAN_POINT ( 'NONE',  ( 0.000000000000000000, 0.000000000000000000, -4.699999999999981526 ) ) ;
#4467=LINE ( 'NONE', #1222, #720 ) ;
#4473=FACE_OUTER_BOUND ( 'NONE', #8579, .T. ) ;
#4502=CARTESIAN_POINT ( 'NONE',  ( 0.1410420225375863257, -4.700232803196146669, -3.387027626239156319 ) ) ;
#4528=DIRECTION ( 'NONE',  ( 0.000000000000000000, 0.000000000000000000, 1.000000000000000000 ) ) ;
#4570=CARTESIAN_POINT ( 'NONE',  ( -0.6666666666666672958, 4.233901974057265427, -3.000726591567076440 ) ) ;
#4571=DIRECTION ( 'NONE',  ( 0.000000000000000000, 0.000000000000000000, 1.000000000000000000 ) ) ;
#4581=EDGE_LOOP ( 'NONE', ( #6415, #6070, #3516, #4003, #5735 ) ) ;
#4592=ORIENTED_EDGE ( 'NONE', *, *, #7191, .F. ) ;
#4596=EDGE_CURVE ( 'NONE', #10542, #3192, #12932, .T. ) ;
#4599=CARTESIAN_POINT ( 'NONE',  ( 0.000000000000000000, 0.000000000000000000, -4.674599999999973221 ) ) ;
#4602=DIRECTION ( 'NONE',  ( 0.000000000000000000, 0.000000000000000000, 1.000000000000000000 ) ) ;
#4605=DIRECTION ( 'NONE',  ( 1.000000000000000000, 1.665334536937734071E-16, 0.000000000000000000 ) ) ;
#4609=CARTESIAN_POINT ( 'NONE',  ( -2.540000000000002700, -1.119346853987568578E-16, 1.599999999999990319 ) ) ;
#4612=ORIENTED_EDGE ( 'NONE', *, *, #10257, .T. ) ;
#4621=PLANE ( 'NONE',  #4281 ) ;
#4645=EDGE_CURVE ( 'NONE', #4911, #7523, #9497, .T. ) ;
#4652=DIRECTION ( 'NONE',  ( 0.000000000000000000, 0.000000000000000000, 1.000000000000000000 ) ) ;
#4657=AXIS2_PLACEMENT_3D ( 'NONE', #11310, #10351, #12607 ) ;
#4661=EDGE_CURVE ( 'NONE', #6344, #11445, #7059, .T. ) ;
#4674=CARTESIAN_POINT ( 'NONE',  ( -4.211399291375520271, 2.459730787265050900, -3.451162385478133476 ) ) ;
#4695=ORIENTED_EDGE ( 'NONE', *, *, #7835, .T. ) ;
#4697=MECHANICAL_DESIGN_GEOMETRIC_PRESENTATION_REPRESENTATION('',(#6068),#5387);
#4713=UNCERTAINTY_MEASURE_WITH_UNIT (LENGTH_MEASURE( 1.000000000000000082E-05 ), #5031, 'distance_accuracy_value', 'NONE');
#4741=CARTESIAN_POINT ( 'NONE',  ( 0.000000000000000000, -4.618802153517030717, -4.699999999999981526 ) ) ;
#4773=EDGE_CURVE ( 'NONE', #2554, #13711, #2135, .T. ) ;
#4781=ORIENTED_EDGE ( 'NONE', *, *, #8707, .T. ) ;
#4782=CARTESIAN_POINT ( 'NONE',  ( -0.6507732100473486714, 4.243078065514781727, -0.2236248678334887274 ) ) ;
#4793=EDGE_CURVE ( 'NONE', #6532, #2424, #10708, .T. ) ;
#4794=CARTESIAN_POINT ( 'NONE',  ( 1.287221018261892169, 3.875624752116891614, -3.130620751971864291 ) ) ;
#4796=CARTESIAN_POINT ( 'NONE',  ( 4.211140560182194292, -2.431303136016548017, -3.445885042887453231 ) ) ;
#4809=CARTESIAN_POINT ( 'NONE',  ( 0.000000000000000000, 0.000000000000000000, 2.400000000000013234 ) ) ;
#4811=CARTESIAN_POINT ( 'NONE',  ( -3.999999999999990674, -1.658477411507763621, -3.231534348143921598 ) ) ;
#4814=CARTESIAN_POINT ( 'NONE',  ( -3.333333333333330817, 2.694301256218247342, -3.000726591567076440 ) ) ;
#4817=EDGE_LOOP ( 'NONE', ( #12123, #8622, #3426, #7107 ) ) ;
#4833=ORIENTED_EDGE ( 'NONE', *, *, #4873, .F. ) ;
#4873=EDGE_CURVE ( 'NONE', #14315, #661, #422, .T. ) ;
#4891=AXIS2_PLACEMENT_3D ( 'NONE', #4116, #12643, #1529 ) ;
#4908=CARTESIAN_POINT ( 'NONE',  ( 4.000000000000000000, 6.661338147750937270E-16, 1.599999999999990319 ) ) ;
#4909=CARTESIAN_POINT ( 'NONE',  ( -4.211140560182201398, -2.431303136016548017, -3.445885042887453231 ) ) ;
#4911=VERTEX_POINT ( 'NONE', #7995 ) ;
#4922=CARTESIAN_POINT ( 'NONE',  ( -1.747541505913280391, 3.837784562140261535, -3.203702292528891604 ) ) ;
#4960=DIRECTION ( 'NONE',  ( 1.000000000000000000, 1.665334536937734071E-16, 0.000000000000000000 ) ) ;
#4973=CARTESIAN_POINT ( 'NONE',  ( -2.500000000000002220, -4.163336342344338999E-16, -4.674599999999973221 ) ) ;
#4989=EDGE_CURVE ( 'NONE', #2424, #13364, #1827, .T. ) ;
#5004=CARTESIAN_POINT ( 'NONE',  ( -0.3461262719736090121, 4.658553426539293163, -3.371615880910392438 ) ) ;
#5016=CARTESIAN_POINT ( 'NONE',  ( 3.453019673806204004, 2.625200315326535971, -3.235259548910409677 ) ) ;
#5031=( LENGTH_UNIT ( ) NAMED_UNIT ( * ) SI_UNIT ( .MILLI., .METRE. ) );
#5086=CIRCLE ( 'NONE', #5763, 3.000000000000001332 ) ;
#5090=EDGE_LOOP ( 'NONE', ( #2347, #10091, #723 ) ) ;
#5092=CARTESIAN_POINT ( 'NONE',  ( 5.560781378645576645, 1.607055439833521515E-15, -3.699999999999981082 ) ) ;
#5128=ADVANCED_FACE ( 'NONE', ( #8210 ), #10636, .T. ) ;
#5140=ORIENTED_EDGE ( 'NONE', *, *, #13248, .F. ) ;
#5169=VECTOR ( 'NONE', #7050, 1000.000000000000114 ) ;
#5179=CARTESIAN_POINT ( 'NONE',  ( 1.828356344711646431, 3.563200125723183120, -4.669316179125290331E-15 ) ) ;
#5180=ORIENTED_EDGE ( 'NONE', *, *, #2187, .T. ) ;
#5192=CARTESIAN_POINT ( 'NONE',  ( -4.207491450040565795, 2.029819825146467416, -3.371670828759588456 ) ) ;
#5202=CARTESIAN_POINT ( 'NONE',  ( -4.101948962585907132, -2.368261337751098594, -3.381124513963619016 ) ) ;
#5204=VECTOR ( 'NONE', #8806, 1000.000000000000000 ) ;
#5234=CARTESIAN_POINT ( 'NONE',  ( 1.747541505913290605, -3.837784562140271305, -3.203702292528895157 ) ) ;
#5237=EDGE_CURVE ( 'NONE', #6553, #11217, #11752, .T. ) ;
#5254=ORIENTED_EDGE ( 'NONE', *, *, #241, .F. ) ;
#5267=CARTESIAN_POINT ( 'NONE',  ( -4.198928548860770604, 0.8158838809860085028, -3.226471437616899252 ) ) ;
#5291=DIRECTION ( 'NONE',  ( 0.7071067811865490160, 1.177569344012833409E-16, 0.7071067811865460184 ) ) ;
#5302=ORIENTED_EDGE ( 'NONE', *, *, #1174, .F. ) ;
#5309=CARTESIAN_POINT ( 'NONE',  ( -3.999999999999995559, 0.1981133338132423372, 1.817203309215693801E-15 ) ) ;
#5312=DIRECTION ( 'NONE',  ( 0.000000000000000000, 0.000000000000000000, -1.000000000000000000 ) ) ;
#5317=CARTESIAN_POINT ( 'NONE',  ( 0.6448876103708376384, 4.246476118072356698, -0.2256878752776751151 ) ) ;
#5319=B_SPLINE_CURVE_WITH_KNOTS ( 'NONE', 3,
 ( #12235, #2276, #9, #1175, #3314, #2215 ),
 .UNSPECIFIED., .F., .F.,
 ( 4, 2, 4 ),
 ( -3.640115492415446757E-06, 0.0002066546034006449238, 0.0004169493222937052960 ),
 .UNSPECIFIED. ) ;
#5329=CARTESIAN_POINT ( 'NONE',  ( 0.000000000000000000, 4.618802153517016507, -0.5000000000000004441 ) ) ;
#5331=CARTESIAN_POINT ( 'NONE',  ( 3.999999999999999112, -1.700153365594969879, -3.020323189000999164 ) ) ;
#5332=EDGE_CURVE ( 'NONE', #11217, #11202, #8031, .T. ) ;
#5341=DIRECTION ( 'NONE',  ( 0.000000000000000000, 0.000000000000000000, 1.000000000000000000 ) ) ;
#5344=DIRECTION ( 'NONE',  ( 0.000000000000000000, 0.000000000000000000, 1.000000000000000000 ) ) ;
#5346=FILL_AREA_STYLE ('',( #7598 ) ) ;
#5354=CARTESIAN_POINT ( 'NONE',  ( -1.287221018261888839, -3.875624752116721528, -3.130620751971867843 ) ) ;
#5367=CARTESIAN_POINT ( 'NONE',  ( 4.175647895129166898, -2.207990717223097921, -3.169390900447838888 ) ) ;
#5368=CONICAL_SURFACE ( 'NONE', #13564, 5.560781378645576645, 1.221730476396047926 ) ;
#5387=( GEOMETRIC_REPRESENTATION_CONTEXT ( 3 ) GLOBAL_UNCERTAINTY_ASSIGNED_CONTEXT ( ( #4713 ) ) GLOBAL_UNIT_ASSIGNED_CONTEXT ( ( #5031, #4105, #4168 ) ) REPRESENTATION_CONTEXT ( 'NONE', 'WORKASPACE' ) );
#5401=DIRECTION ( 'NONE',  ( 0.5000000000000009992, -0.8660254037844380415, 0.000000000000000000 ) ) ;
#5404=CARTESIAN_POINT ( 'NONE',  ( 3.999999999999999112, -2.471526491860384311, -3.386887032901821470 ) ) ;
#5421=CONICAL_SURFACE ( 'NONE', #14314, 4.000000000000000000, 0.8911886515913775009 ) ;
#5431=CARTESIAN_POINT ( 'NONE',  ( 4.000000000000003553, -1.539600717839009203, -3.000726591567076440 ) ) ;
#5441=DIRECTION ( 'NONE',  ( 1.000000000000000000, 0.000000000000000000, 0.000000000000000000 ) ) ;
#5447=CARTESIAN_POINT ( 'NONE',  ( -1.391697335622804621, -4.043246145443390560, -3.203898532754352768 ) ) ;
#5449=FACE_OUTER_BOUND ( 'NONE', #8596, .T. ) ;
#5467=DIRECTION ( 'NONE',  ( 1.000000000000000000, 1.665334536937734071E-16, 0.000000000000000000 ) ) ;
#5499=DIRECTION ( 'NONE',  ( 0.000000000000000000, 0.000000000000000000, 1.000000000000000000 ) ) ;
#5503=CARTESIAN_POINT ( 'NONE',  ( -3.999999999999996447, 2.309401076758494487, -4.699999999999981526 ) ) ;
#5516=ORIENTED_EDGE ( 'NONE', *, *, #13533, .T. ) ;
#5520=DIRECTION ( 'NONE',  ( 1.000000000000000000, 1.665334536937734071E-16, 0.000000000000000000 ) ) ;
#5521=CARTESIAN_POINT ( 'NONE',  ( -3.999999999999996447, -2.309401076758511806, -0.5000000000000004441 ) ) ;
#5545=ADVANCED_FACE ( 'NONE', ( #6208 ), #5368, .T. ) ;
#5555=CARTESIAN_POINT ( 'NONE',  ( 0.000000000000000000, 0.000000000000000000, 2.400000000000013234 ) ) ;
#5586=CARTESIAN_POINT ( 'NONE',  ( 2.888823775385669489E-13, -4.796980096169635388, -3.421999068284433676 ) ) ;
#5609=CARTESIAN_POINT ( 'NONE',  ( 4.211140560182194292, -2.431303136016548017, -3.445885042887453231 ) ) ;
#5667=ORIENTED_EDGE ( 'NONE', *, *, #2431, .F. ) ;
#5676=CARTESIAN_POINT ( 'NONE',  ( 0.000000000000000000, 0.000000000000000000, -4.674599999999973221 ) ) ;
#5677=CARTESIAN_POINT ( 'NONE',  ( -3.000000000000000000, -1.322063213371142838E-16, 2.400000000000013234 ) ) ;
#5681=EDGE_CURVE ( 'NONE', #3192, #11427, #4467, .T. ) ;
#5682=EDGE_CURVE ( 'NONE', #7559, #13013, #7195, .T. ) ;
#5686=CARTESIAN_POINT ( 'NONE',  ( -1.360615521533644401, 4.061278559078192352, -3.205052026701860513 ) ) ;
#5689=DIRECTION ( 'NONE',  ( -0.000000000000000000, -0.000000000000000000, 1.000000000000000000 ) ) ;
#5706=ADVANCED_FACE ( 'NONE', ( #11530 ), #1357, .T. ) ;
#5735=ORIENTED_EDGE ( 'NONE', *, *, #11672, .F. ) ;
#5740=AXIS2_PLACEMENT_3D ( 'NONE', #5503, #961, #11136 ) ;
#5762=AXIS2_PLACEMENT_3D ( 'NONE', #6523, #2010, #6450 ) ;
#5763=AXIS2_PLACEMENT_3D ( 'NONE', #4809, #10153, #6917 ) ;
#5771=AXIS2_PLACEMENT_3D ( 'NONE', #3317, #14365, #2059 ) ;
#5774=ORIENTED_EDGE ( 'NONE', *, *, #13636, .F. ) ;
#5786=CARTESIAN_POINT ( 'NONE',  ( 5.560781378645534900, 9.260561282218635514E-16, -3.699999999999981082 ) ) ;
#5798=ORIENTED_EDGE ( 'NONE', *, *, #987, .T. ) ;
#5816=CARTESIAN_POINT ( 'NONE',  ( -4.175647895129166898, 2.207990717223085486, -3.169390900447837112 ) ) ;
#5828=CARTESIAN_POINT ( 'NONE',  ( 4.000000000000003553, 2.309401076758501592, -4.699999999999981526 ) ) ;
#5832=ORIENTED_EDGE ( 'NONE', *, *, #1775, .F. ) ;
#5898=CARTESIAN_POINT ( 'NONE',  ( -3.436326524993375209, 2.634838109288609509, -3.231543764078446568 ) ) ;
#5910=CARTESIAN_POINT ( 'NONE',  ( 0.6507732100473498926, -4.243078065514795938, -0.2236248678334991080 ) ) ;
#5932=DIRECTION ( 'NONE',  ( 0.000000000000000000, 0.000000000000000000, -1.000000000000000000 ) ) ;
#5937=ADVANCED_FACE ( 'NONE', ( #5449 ), #3755, .F. ) ;
#5943=CARTESIAN_POINT ( 'NONE',  ( -3.999999999999996447, 2.309401076758494487, -4.699999999999981526 ) ) ;
#5951=ORIENTED_EDGE ( 'NONE', *, *, #299, .F. ) ;
#5954=CARTESIAN_POINT ( 'NONE',  ( 4.000000000000003553, 2.309401076758501592, -4.699999999999981526 ) ) ;
#5962=CARTESIAN_POINT ( 'NONE',  ( -3.999999999999991118, 1.677751148815752824, -3.235249634002968833 ) ) ;
#5965=CARTESIAN_POINT ( 'NONE',  ( 1.503496978826011311E-15, 4.647089433458768681, -3.272167766733379946 ) ) ;
#6013=CARTESIAN_POINT ( 'NONE',  ( -3.999999999999996447, -2.309401076758511806, -0.5000000000000004441 ) ) ;
#6014=CARTESIAN_POINT ( 'NONE',  ( 0.5636734750057210697, 4.293365120987118644, -3.231543764078432357 ) ) ;
#6027=CARTESIAN_POINT ( 'NONE',  ( -3.333333333333332593, -2.694301256218264218, -3.000726591567075552 ) ) ;
#6038=CARTESIAN_POINT ( 'NONE',  ( -4.203934431905765656, -1.640681339110420023, -3.298434044919953401 ) ) ;
#6050=DIRECTION ( 'NONE',  ( 0.000000000000000000, 0.000000000000000000, 1.000000000000000000 ) ) ;
#6068=STYLED_ITEM ( 'NONE', ( #7212 ), #11581 ) ;
#6070=ORIENTED_EDGE ( 'NONE', *, *, #2431, .T. ) ;
#6094=DIRECTION ( 'NONE',  ( 0.000000000000000000, 0.000000000000000000, 1.000000000000000000 ) ) ;
#6096=CARTESIAN_POINT ( 'NONE',  ( 4.000000000000003553, -2.309401076758511806, -3.133295621305376422 ) ) ;
#6125=CARTESIAN_POINT ( 'NONE',  ( 2.100000000000000977, 3.497202527569243497E-16, -4.699999999999981526 ) ) ;
#6148=CARTESIAN_POINT ( 'NONE',  ( -4.000000000000000000, -2.309401076758511806, -3.133295621305376422 ) ) ;
#6150=CIRCLE ( 'NONE', #93, 3.000000000000001332 ) ;
#6158=DIRECTION ( 'NONE',  ( -1.000000000000000000, -1.665334536937734071E-16, 0.000000000000000000 ) ) ;
#6172=ORIENTED_EDGE ( 'NONE', *, *, #2508, .T. ) ;
#6181=CARTESIAN_POINT ( 'NONE',  ( 0.3461262719736172833, -4.658553426539298492, -3.371615880910392882 ) ) ;
#6201=CYLINDRICAL_SURFACE ( 'NONE', #12350, 3.000000000000001332 ) ;
#6208=FACE_OUTER_BOUND ( 'NONE', #12925, .T. ) ;
#6238=CARTESIAN_POINT ( 'NONE',  ( 0.000000000000000000, 4.618802153517016507, -3.133295621305376422 ) ) ;
#6241=DIRECTION ( 'NONE',  ( 0.000000000000000000, 0.000000000000000000, -1.000000000000000000 ) ) ;
#6245=ORIENTED_EDGE ( 'NONE', *, *, #9223, .F. ) ;
#6263=VECTOR ( 'NONE', #1548, 1000.000000000000000 ) ;
#6266=CARTESIAN_POINT ( 'NONE',  ( 0.000000000000000000, 4.618802153517016507, -0.5000000000000004441 ) ) ;
#6282=CARTESIAN_POINT ( 'NONE',  ( 0.000000000000000000, 4.862606272033096033, -3.445885042887453231 ) ) ;
#6322=CARTESIAN_POINT ( 'NONE',  ( -0.1750032273043237441, -4.719840313910227181, -3.169254239516205107 ) ) ;
#6342=ORIENTED_EDGE ( 'NONE', *, *, #9212, .T. ) ;
#6344=VERTEX_POINT ( 'NONE', #7773 ) ;
#6354=CARTESIAN_POINT ( 'NONE',  ( 3.861362476283259237, 2.629030857715991321, -3.371615880910392882 ) ) ;
#6361=DIRECTION ( 'NONE',  ( -0.000000000000000000, -0.000000000000000000, 1.000000000000000000 ) ) ;
#6408=SURFACE_SIDE_STYLE ('',( #11606 ) ) ;
#6415=ORIENTED_EDGE ( 'NONE', *, *, #3513, .T. ) ;
#6417=EDGE_CURVE ( 'NONE', #13711, #2554, #13098, .T. ) ;
#6432=ORIENTED_EDGE ( 'NONE', *, *, #2623, .T. ) ;
#6437=CARTESIAN_POINT ( 'NONE',  ( -3.540000644887378645, -2.810673041921230020, -3.302142222889056455 ) ) ;
#6438=PRODUCT_DEFINITION_CONTEXT ( 'detailed design', #645, 'design' ) ;
#6450=DIRECTION ( 'NONE',  ( 0.8660254037844378194, -0.5000000000000014433, 0.000000000000000000 ) ) ;
#6451=CARTESIAN_POINT ( 'NONE',  ( 1.360615521534842998, -4.061278559077564410, -3.205052026701877388 ) ) ;
#6455=DIRECTION ( 'NONE',  ( 1.000000000000000000, 1.665334536937734071E-16, 0.000000000000000000 ) ) ;
#6471=AXIS2_PLACEMENT_3D ( 'NONE', #478, #1797, #12929 ) ;
#6474=ORIENTED_EDGE ( 'NONE', *, *, #12008, .T. ) ;
#6499=VECTOR ( 'NONE', #12553, 1000.000000000000000 ) ;
#6500=CARTESIAN_POINT ( 'NONE',  ( 0.000000000000000000, 0.000000000000000000, 1.599999999999990319 ) ) ;
#6504=( NAMED_UNIT ( * ) PLANE_ANGLE_UNIT ( ) SI_UNIT ( $, .RADIAN. ) );
#6513=CIRCLE ( 'NONE', #2097, 5.560781378645576645 ) ;
#6521=DIRECTION ( 'NONE',  ( -1.000000000000000000, -1.665334536937734071E-16, -0.000000000000000000 ) ) ;
#6523=CARTESIAN_POINT ( 'NONE',  ( -4.000000000000000000, -2.309401076758511806, -4.699999999999981526 ) ) ;
#6524=DIRECTION ( 'NONE',  ( 0.000000000000000000, 0.000000000000000000, 1.000000000000000000 ) ) ;
#6529=( BOUNDED_SURFACE ( )  B_SPLINE_SURFACE ( 3, 2, ( 
 ( #2552, #12293, #1237 ),
 ( #13758, #12503, #1369 ),
 ( #3444, #2269, #5686 ),
 ( #10162, #145, #13543 ),
 ( #3515, #5898, #6714 ),
 ( #5816, #2408, #6867 ) ),
 .UNSPECIFIED., .F., .F., .F. ) 
 B_SPLINE_SURFACE_WITH_KNOTS ( ( 4, 2, 4 ),
 ( 3, 3 ),
 ( 0.02023740217035200836, 0.02269762987400599646, 0.02515785757765998457 ),
 ( 0.000000000000000000, 1.000000000000000000 ),
 .UNSPECIFIED. ) 
 GEOMETRIC_REPRESENTATION_ITEM ( )  RATIONAL_B_SPLINE_SURFACE ( (
 ( 1.000000000000000000, 0.8047781539129729156, 1.000000000000000000),
 ( 1.000000000000000000, 0.8123770319056065059, 1.000000000000000000),
 ( 1.000000000000000000, 0.8190663783058289571, 1.000000000000000000),
 ( 1.000000000000000000, 0.8192359702875615657, 1.000000000000000000),
 ( 1.000000000000000000, 0.8126134888420907254, 1.000000000000000000),
 ( 1.000000000000000000, 0.8047712368238109093, 1.000000000000000000) ) ) 
 REPRESENTATION_ITEM ( '' )  SURFACE ( )  );
#6532=VERTEX_POINT ( 'NONE', #12725 ) ;
#6540=CARTESIAN_POINT ( 'NONE',  ( 0.000000000000000000, 0.000000000000000000, -3.699999999999981082 ) ) ;
#6546=AXIS2_PLACEMENT_3D ( 'NONE', #7063, #2402, #12496 ) ;
#6553=VERTEX_POINT ( 'NONE', #802 ) ;
#6563=CARTESIAN_POINT ( 'NONE',  ( 4.024499207728660544, -2.323545700935590652, -3.272172305156503480 ) ) ;
#6564=VECTOR ( 'NONE', #682, 1000.000000000000000 ) ;
#6570=AXIS2_PLACEMENT_3D ( 'NONE', #3392, #7828, #2137 ) ;
#6604=CIRCLE ( 'NONE', #10819, 5.560781378645576645 ) ;
#6607=DIRECTION ( 'NONE',  ( 0.000000000000000000, 0.000000000000000000, 1.000000000000000000 ) ) ;
#6608=ORIENTED_EDGE ( 'NONE', *, *, #5681, .F. ) ;
#6609=FACE_OUTER_BOUND ( 'NONE', #9466, .T. ) ;
#6612=AXIS2_PLACEMENT_3D ( 'NONE', #11806, #11950, #7604 ) ;
#6616=CARTESIAN_POINT ( 'NONE',  ( -2.369796611257730795E-32, -4.618802153517031606, -3.204271511726780375 ) ) ;
#6649=CARTESIAN_POINT ( 'NONE',  ( 2.000000000000001776, -3.464101615137764156, 0.000000000000000000 ) ) ;
#6657=CARTESIAN_POINT ( 'NONE',  ( 0.000000000000000000, 0.000000000000000000, 1.159999999999994369 ) ) ;
#6672=ORIENTED_EDGE ( 'NONE', *, *, #11672, .T. ) ;
#6690=ORIENTED_EDGE ( 'NONE', *, *, #4773, .T. ) ;
#6696=EDGE_LOOP ( 'NONE', ( #13422, #4781, #6245, #9411 ) ) ;
#6710=CIRCLE ( 'NONE', #13738, 0.7999999999999999334 ) ;
#6714=CARTESIAN_POINT ( 'NONE',  ( -3.522881874162831828, 2.820349071481866421, -3.298443181296048188 ) ) ;
#6719=FACE_OUTER_BOUND ( 'NONE', #3825, .T. ) ;
#6733=CIRCLE ( 'NONE', #2300, 5.384454397937120440 ) ;
#6741=FACE_OUTER_BOUND ( 'NONE', #8783, .T. ) ;
#6746=ORIENTED_EDGE ( 'NONE', *, *, #12141, .T. ) ;
#6751=PLANE ( 'NONE',  #1033 ) ;
#6759=EDGE_CURVE ( 'NONE', #12258, #2748, #6513, .T. ) ;
#6774=CARTESIAN_POINT ( 'NONE',  ( -2.000000000000001776, -3.464101615137750390, 0.000000000000000000 ) ) ;
#6799=CARTESIAN_POINT ( 'NONE',  ( 2.687328764639632883, -3.067272167851310627, -0.05923475698271751799 ) ) ;
#6823=ORIENTED_EDGE ( 'NONE', *, *, #13424, .T. ) ;
#6839=CONICAL_SURFACE ( 'NONE', #13404, 4.000000000000000000, 0.8911886515913775009 ) ;
#6867=CARTESIAN_POINT ( 'NONE',  ( -4.236525418537980592, 2.416953631397924074, -3.451298686683611283 ) ) ;
#6869=VERTEX_POINT ( 'NONE', #8536 ) ;
#6905=ADVANCED_FACE ( 'NONE', ( #6719 ), #4436, .T. ) ;
#6911=VERTEX_POINT ( 'NONE', #6649 ) ;
#6917=DIRECTION ( 'NONE',  ( 1.000000000000000000, 1.665334536937734318E-16, 0.000000000000000000 ) ) ;
#6921=DIRECTION ( 'NONE',  ( 0.000000000000000000, 0.000000000000000000, 1.000000000000000000 ) ) ;
#6951=CARTESIAN_POINT ( 'NONE',  ( -2.500000000000000888, -1.101719344475952406E-16, -4.699999999999981526 ) ) ;
#6952=CIRCLE ( 'NONE', #9055, 2.500000000000002220 ) ;
#6971=CARTESIAN_POINT ( 'NONE',  ( 0.5449245075113242631, 4.304189842417321721, -3.016622336521755265 ) ) ;
#6979=CARTESIAN_POINT ( 'NONE',  ( 0.000000000000000000, -4.618802153517030717, -3.133295621305376422 ) ) ;
#6991=FACE_OUTER_BOUND ( 'NONE', #13888, .T. ) ;
#7001=EDGE_LOOP ( 'NONE', ( #11447, #13485, #2315, #9106, #3342, #317 ) ) ;
#7020=B_SPLINE_CURVE_WITH_KNOTS ( 'NONE', 3,
 ( #7055, #6027, #3934, #9258, #6979 ),
 .UNSPECIFIED., .F., .F.,
 ( 4, 1, 4 ),
 ( 0.000000000000000000, 0.002309401076758506657, 0.004618802153517013315 ),
 .UNSPECIFIED. ) ;
#7030=VECTOR ( 'NONE', #2434, 999.9999999999998863 ) ;
#7033=PLANE ( 'NONE',  #3535 ) ;
#7045=CARTESIAN_POINT ( 'NONE',  ( -0.1756478951291627899, 4.720212513052423731, -3.169390900447838000 ) ) ;
#7050=DIRECTION ( 'NONE',  ( -0.8191520442889900222, -1.364162190357603728E-16, -0.5735764363510484909 ) ) ;
#7055=CARTESIAN_POINT ( 'NONE',  ( -4.000000000000000000, -2.309401076758511806, -3.133295621305376422 ) ) ;
#7057=CARTESIAN_POINT ( 'NONE',  ( 3.349226789952655992, 2.685125164760735039, -0.2236248678334833151 ) ) ;
#7059=CIRCLE ( 'NONE', #1466, 2.100000000000000977 ) ;
#7063=CARTESIAN_POINT ( 'NONE',  ( 0.000000000000000000, 0.000000000000000000, 0.000000000000000000 ) ) ;
#7094=( NAMED_UNIT ( * ) PLANE_ANGLE_UNIT ( ) SI_UNIT ( $, .RADIAN. ) );
#7107=ORIENTED_EDGE ( 'NONE', *, *, #7274, .F. ) ;
#7118=CARTESIAN_POINT ( 'NONE',  ( -0.1410420225375824677, 4.700232803196133347, -3.387027626239151434 ) ) ;
#7122=VERTEX_POINT ( 'NONE', #9853 ) ;
#7134=FILL_AREA_STYLE ('',( #10515 ) ) ;
#7137=CARTESIAN_POINT ( 'NONE',  ( -3.999999999999991118, -0.8232522521399826543, -3.130632262998142235 ) ) ;
#7141=ORIENTED_EDGE ( 'NONE', *, *, #7659, .F. ) ;
#7175=DIRECTION ( 'NONE',  ( -1.000000000000000000, -1.665334536937734071E-16, -0.000000000000000000 ) ) ;
#7179=EDGE_CURVE ( 'NONE', #13364, #14315, #8730, .T. ) ;
#7191=EDGE_CURVE ( 'NONE', #11970, #4249, #13051, .T. ) ;
#7192=CARTESIAN_POINT ( 'NONE',  ( 0.6810530063608244422, 4.461079733297845351, -3.298443181296111248 ) ) ;
#7194=CARTESIAN_POINT ( 'NONE',  ( 0.6937372685066715006, -4.453844082567738560, -3.310536846335876859 ) ) ;
#7195=B_SPLINE_CURVE_WITH_KNOTS ( 'NONE', 3,
 ( #493, #9183, #3791, #7057, #1578, #13680 ),
 .UNSPECIFIED., .F., .F.,
 ( 4, 2, 4 ),
 ( 0.002365888236227995517, 0.003551327329835083681, 0.004736766423442171844 ),
 .UNSPECIFIED. ) ;
#7199=B_SPLINE_CURVE_WITH_KNOTS ( 'NONE', 3,
 ( #11055, #8850, #948, #2133, #10024 ),
 .UNSPECIFIED., .F., .F.,
 ( 4, 1, 4 ),
 ( 0.000000000000000000, 0.002309401076758505790, 0.004618802153517011580 ),
 .UNSPECIFIED. ) ;
#7212=PRESENTATION_STYLE_ASSIGNMENT (( #496 ) ) ;
#7219=CARTESIAN_POINT ( 'NONE',  ( 4.000000000000004441, -0.3979232138631220717, -4.518073740654438009E-15 ) ) ;
#7220=EDGE_LOOP ( 'NONE', ( #2210, #14387 ) ) ;
#7271=CARTESIAN_POINT ( 'NONE',  ( 2.756166666307359847, 3.027528586792976650, -2.923144239647418541 ) ) ;
#7274=EDGE_CURVE ( 'NONE', #13002, #2748, #2083, .T. ) ;
#7276=CARTESIAN_POINT ( 'NONE',  ( -3.999999999999996447, 2.309401076758494487, -3.133295621305376422 ) ) ;
#7292=AXIS2_PLACEMENT_3D ( 'NONE', #10920, #6241, #6521 ) ;
#7320=ORIENTED_EDGE ( 'NONE', *, *, #7191, .T. ) ;
#7330=FACE_OUTER_BOUND ( 'NONE', #4017, .T. ) ;
#7333=CARTESIAN_POINT ( 'NONE',  ( 3.999999999999993339, -5.421010862427522170E-15, -2.842992957459210324 ) ) ;
#7355=EDGE_LOOP ( 'NONE', ( #1141, #7320, #2678, #4175 ) ) ;
#7359=ORIENTED_EDGE ( 'NONE', *, *, #6417, .T. ) ;
#7368=CARTESIAN_POINT ( 'NONE',  ( 0.3198814748697595411, 4.434118497892185040, -0.3507732604232542406 ) ) ;
#7373=EDGE_LOOP ( 'NONE', ( #7452, #14388, #5180, #5516, #11667, #4592 ) ) ;
#7382=CARTESIAN_POINT ( 'NONE',  ( -4.211140560182194292, 2.431303136016534250, -3.445885042887453231 ) ) ;
#7392=ORIENTED_EDGE ( 'NONE', *, *, #5237, .F. ) ;
#7412=CARTESIAN_POINT ( 'NONE',  ( 2.500000000000002220, 4.163336342344338999E-16, -25.03750572909319061 ) ) ;
#7430=AXIS2_PLACEMENT_3D ( 'NONE', #6540, #5312, #13228 ) ;
#7452=ORIENTED_EDGE ( 'NONE', *, *, #13807, .F. ) ;
#7464=FACE_OUTER_BOUND ( 'NONE', #8096, .T. ) ;
#7475=CARTESIAN_POINT ( 'NONE',  ( 0.5469803261926681204, -4.303002914946961077, -3.235259548911087357 ) ) ;
#7493=EDGE_LOOP ( 'NONE', ( #1650, #9785, #3756, #1662, #11873, #9328, #2353 ) ) ;
#7515=CARTESIAN_POINT ( 'NONE',  ( 3.999999999999998224, 2.472263363263131009, -3.387027814857410224 ) ) ;
#7523=VERTEX_POINT ( 'NONE', #9756 ) ;
#7536=VERTEX_POINT ( 'NONE', #14307 ) ;
#7559=VERTEX_POINT ( 'NONE', #10046 ) ;
#7563=EDGE_LOOP ( 'NONE', ( #4338, #12537, #11369, #2984 ) ) ;
#7578=DIRECTION ( 'NONE',  ( -0.000000000000000000, -0.000000000000000000, -1.000000000000000000 ) ) ;
#7583=CARTESIAN_POINT ( 'NONE',  ( 0.000000000000000000, -4.618802153517030717, -4.699999999999981526 ) ) ;
#7591=ORIENTED_EDGE ( 'NONE', *, *, #10402, .F. ) ;
#7598=FILL_AREA_STYLE_COLOUR ( '', #4020 ) ;
#7599=ADVANCED_FACE ( 'NONE', ( #13148 ), #12037, .T. ) ;
#7604=DIRECTION ( 'NONE',  ( -1.000000000000000000, -1.665334536937734071E-16, 0.000000000000000000 ) ) ;
#7617=VERTEX_POINT ( 'NONE', #10250 ) ;
#7631=DIRECTION ( 'NONE',  ( 0.000000000000000000, 0.000000000000000000, 1.000000000000000000 ) ) ;
#7652=CARTESIAN_POINT ( 'NONE',  ( 2.100000000000000089, 3.497202527569242018E-16, -4.394516984716101859 ) ) ;
#7659=EDGE_CURVE ( 'NONE', #9307, #10589, #11218, .T. ) ;
#7672=SURFACE_STYLE_FILL_AREA ( #5346 ) ;
#7684=CARTESIAN_POINT ( 'NONE',  ( -1.274241539467172002, -3.883118457693044423, -2.920601398289143003 ) ) ;
#7694=PLANE ( 'NONE',  #7292 ) ;
#7695=EDGE_LOOP ( 'NONE', ( #5832, #2407, #14252, #11921 ) ) ;
#7727=VERTEX_POINT ( 'NONE', #12742 ) ;
#7731=AXIS2_PLACEMENT_3D ( 'NONE', #11337, #9208, #3600 ) ;
#7737=ORIENTED_EDGE ( 'NONE', *, *, #7274, .T. ) ;
#7738=B_SPLINE_CURVE_WITH_KNOTS ( 'NONE', 3,
 ( #4909, #11637, #5202, #1698, #11942, #6148 ),
 .UNSPECIFIED., .F., .F.,
 ( 4, 2, 4 ),
 ( -3.640115492426956241E-06, 0.0002066546034006362231, 0.0004169493222936994413 ),
 .UNSPECIFIED. ) ;
#7760=AXIS2_PLACEMENT_3D ( 'NONE', #10021, #5344, #8921 ) ;
#7765=CARTESIAN_POINT ( 'NONE',  ( 0.000000000000000000, 0.000000000000000000, 0.000000000000000000 ) ) ;
#7768=CARTESIAN_POINT ( 'NONE',  ( -2.836862643238879489, -3.208966885971408445, -3.205052026701902257 ) ) ;
#7773=CARTESIAN_POINT ( 'NONE',  ( -2.100000000000000089, -9.254442493598001840E-17, -4.394516984716101859 ) ) ;
#7791=CIRCLE ( 'NONE', #3378, 2.500000000000002220 ) ;
#7828=DIRECTION ( 'NONE',  ( 0.000000000000000000, 0.000000000000000000, 1.000000000000000000 ) ) ;
#7834=CARTESIAN_POINT ( 'NONE',  ( -2.742797192660130001, -3.035247456002393651, -3.133250573521596749 ) ) ;
#7835=EDGE_CURVE ( 'NONE', #13588, #2847, #1620, .T. ) ;
#7849=DIRECTION ( 'NONE',  ( -1.000000000000000000, -1.665334536937734071E-16, 0.000000000000000000 ) ) ;
#7855=CARTESIAN_POINT ( 'NONE',  ( 0.000000000000000000, -4.862606272033103139, -3.445885042887453231 ) ) ;
#7858=ADVANCED_FACE ( 'NONE', ( #4426 ), #13287, .T. ) ;
#7889=ORIENTED_EDGE ( 'NONE', *, *, #5332, .F. ) ;
#7894=CARTESIAN_POINT ( 'NONE',  ( 2.000000000000001776, -3.464101615137764156, 0.000000000000000000 ) ) ;
#7914=CARTESIAN_POINT ( 'NONE',  ( 0.000000000000000000, 0.000000000000000000, 1.599999999999990319 ) ) ;
#7920=AXIS2_PLACEMENT_3D ( 'NONE', #103, #2712, #9284 ) ;
#7946=CARTESIAN_POINT ( 'NONE',  ( 0.000000000000000000, 0.000000000000000000, 2.400000000000013234 ) ) ;
#7995=CARTESIAN_POINT ( 'NONE',  ( 4.211140560182201398, 2.431303136016537358, -3.445885042887453231 ) ) ;
#8006=ORIENTED_EDGE ( 'NONE', *, *, #9223, .T. ) ;
#8025=AXIS2_PLACEMENT_3D ( 'NONE', #4599, #57, #13525 ) ;
#8031=LINE ( 'NONE', #2555, #1171 ) ;
#8032=ADVANCED_FACE ( 'NONE', ( #2777 ), #10439, .F. ) ;
#8040=CARTESIAN_POINT ( 'NONE',  ( 3.000000000000001332, 4.996003610813205418E-16, 13.31572692736082786 ) ) ;
#8050=LINE ( 'NONE', #12462, #7030 ) ;
#8052=EDGE_CURVE ( 'NONE', #1916, #11217, #592, .T. ) ;
#8062=CARTESIAN_POINT ( 'NONE',  ( -2.221569714340160529E-16, -4.736529461165888577, -3.381130640444264479 ) ) ;
#8068=CARTESIAN_POINT ( 'NONE',  ( 2.836862643238862614, 3.208966885971173078, -3.205052026701826318 ) ) ;
#8079=EDGE_CURVE ( 'NONE', #11217, #698, #4089, .T. ) ;
#8082=LINE ( 'NONE', #4741, #6499 ) ;
#8085=LINE ( 'NONE', #4609, #10773 ) ;
#8092=ORIENTED_EDGE ( 'NONE', *, *, #10125, .T. ) ;
#8096=EDGE_LOOP ( 'NONE', ( #7591, #12982, #78, #6690 ) ) ;
#8099=CARTESIAN_POINT ( 'NONE',  ( 4.197393957002307552, 7.823395958202418729E-14, -3.203767560748914445 ) ) ;
#8105=CARTESIAN_POINT ( 'NONE',  ( -1.387778780781445676E-14, -4.618802153517016507, -0.5000000000000004441 ) ) ;
#8118=ORIENTED_EDGE ( 'NONE', *, *, #382, .T. ) ;
#8123=EDGE_CURVE ( 'NONE', #11544, #1594, #8605, .T. ) ;
#8127=ORIENTED_EDGE ( 'NONE', *, *, #12008, .F. ) ;
#8129=CARTESIAN_POINT ( 'NONE',  ( -0.3208286057739688779, 4.433571671609684017, -0.3503314178412602620 ) ) ;
#8144=CARTESIAN_POINT ( 'NONE',  ( 3.511755186886754476, -2.826662030176371410, -3.297382984111599580 ) ) ;
#8146=CARTESIAN_POINT ( 'NONE',  ( -3.999999999999982681, -8.023096076392732812E-15, -2.842992957459206771 ) ) ;
#8151=EDGE_LOOP ( 'NONE', ( #2630, #6432, #8006, #1940 ) ) ;
#8159=EDGE_CURVE ( 'NONE', #11202, #7559, #9277, .T. ) ;
#8167=DIRECTION ( 'NONE',  ( 0.000000000000000000, 0.000000000000000000, 1.000000000000000000 ) ) ;
#8170=CARTESIAN_POINT ( 'NONE',  ( 4.154306624730762287, 2.398490048085581083, -3.421999068284434120 ) ) ;
#8177=ADVANCED_FACE ( 'NONE', ( #9500 ), #6201, .F. ) ;
#8207=CARTESIAN_POINT ( 'NONE',  ( 0.000000000000000000, 4.618802153517016507, -0.5000000000000004441 ) ) ;
#8210=FACE_OUTER_BOUND ( 'NONE', #340, .T. ) ;
#8219=CARTESIAN_POINT ( 'NONE',  ( 4.175003227304316944, 2.208362916365297135, -3.169254239516197114 ) ) ;
#8250=CARTESIAN_POINT ( 'NONE',  ( -1.144235203016676250, -3.958177651039096911, -0.09382832055446391206 ) ) ;
#8257=CARTESIAN_POINT ( 'NONE',  ( 1.391697335622811948, 4.043246145443379014, -3.203898532754351436 ) ) ;
#8265=CARTESIAN_POINT ( 'NONE',  ( -3.680118525130247953, 2.494084732383337055, -0.3507732604232524642 ) ) ;
#8301=LINE ( 'NONE', #5092, #866 ) ;
#8306=CARTESIAN_POINT ( 'NONE',  ( 0.000000000000000000, 0.000000000000000000, 0.000000000000000000 ) ) ;
#8317=CARTESIAN_POINT ( 'NONE',  ( -3.999999999999996447, 1.563622288139188354, -0.2253451193528278329 ) ) ;
#8325=( BOUNDED_SURFACE ( )  B_SPLINE_SURFACE ( 3, 2, ( 
 ( #3802, #10221, #4674 ),
 ( #10374, #5962, #203 ),
 ( #10518, #2698, #2472 ),
 ( #10436, #7137, #424 ),
 ( #13615, #4811, #6038 ),
 ( #11462, #13900, #10291 ) ),
 .UNSPECIFIED., .F., .F., .T. ) 
 B_SPLINE_SURFACE_WITH_KNOTS ( ( 4, 2, 4 ),
 ( 3, 3 ),
 ( 0.02018906359535397113, 0.02264947622839650482, 0.02510988886143903503 ),
 ( 0.000000000000000000, 1.000000000000000000 ),
 .UNSPECIFIED. ) 
 GEOMETRIC_REPRESENTATION_ITEM ( )  RATIONAL_B_SPLINE_SURFACE ( (
 ( 1.000000000000000000, 0.8047781357041526862, 1.000000000000000000),
 ( 1.000000000000000000, 0.8123775905861532198, 1.000000000000000000),
 ( 1.000000000000000000, 0.8190671519372876297, 1.000000000000000000),
 ( 1.000000000000000000, 0.8192352278312100555, 1.000000000000000000),
 ( 1.000000000000000000, 0.8126131206996278777, 1.000000000000000000),
 ( 1.000000000000000000, 0.8047712494894333490, 1.000000000000000000) ) ) 
 REPRESENTATION_ITEM ( '' )  SURFACE ( )  );
#8344=ORIENTED_EDGE ( 'NONE', *, *, #10257, .F. ) ;
#8381=DIRECTION ( 'NONE',  ( 0.9396926207859144231, 2.715694135728174035E-16, -0.3420201433256524481 ) ) ;
#8389=ORIENTED_EDGE ( 'NONE', *, *, #5237, .T. ) ;
#8397=CARTESIAN_POINT ( 'NONE',  ( -2.000000000000001776, -3.464101615137750390, 0.000000000000000000 ) ) ;
#8404=B_SPLINE_CURVE_WITH_KNOTS ( 'NONE', 3,
 ( #9840, #4096, #14244, #14389, #3195, #8743 ),
 .UNSPECIFIED., .F., .F.,
 ( 4, 2, 4 ),
 ( 0.002452478801916362430, 0.003676905084147999610, 0.004901331366379636789 ),
 .UNSPECIFIED. ) ;
#8409=ORIENTED_EDGE ( 'NONE', *, *, #3124, .F. ) ;
#8410=ORIENTED_EDGE ( 'NONE', *, *, #4773, .F. ) ;
#8429=CARTESIAN_POINT ( 'NONE',  ( 0.000000000000000000, 0.000000000000000000, 1.599999999999990319 ) ) ;
#8432=ORIENTED_EDGE ( 'NONE', *, *, #1152, .T. ) ;
#8442=ORIENTED_EDGE ( 'NONE', *, *, #5682, .T. ) ;
#8454=EDGE_LOOP ( 'NONE', ( #6608, #1540, #13407, #3149 ) ) ;
#8488=AXIS2_PLACEMENT_3D ( 'NONE', #13009, #8740, #6455 ) ;
#8491=EDGE_CURVE ( 'NONE', #7727, #1356, #3539, .T. ) ;
#8509=CARTESIAN_POINT ( 'NONE',  ( 4.000000000000003553, -2.309401076758511806, -3.133295621305376422 ) ) ;
#8518=DIRECTION ( 'NONE',  ( -1.000000000000000000, -1.665334536937734071E-16, 0.000000000000000000 ) ) ;
#8536=CARTESIAN_POINT ( 'NONE',  ( 2.500000000000002220, 7.224953340212723619E-16, -4.674599999999973221 ) ) ;
#8566=EDGE_CURVE ( 'NONE', #11544, #6869, #1729, .T. ) ;
#8571=EDGE_CURVE ( 'NONE', #4249, #14186, #6710, .T. ) ;
#8579=EDGE_LOOP ( 'NONE', ( #4612, #13877, #3353, #9448, #5302 ) ) ;
#8594=CARTESIAN_POINT ( 'NONE',  ( -0.6920835326022490852, -4.454600218803899558, -3.297382984111598692 ) ) ;
#8596=EDGE_LOOP ( 'NONE', ( #8127, #12236, #7359, #8634 ) ) ;
#8603=EDGE_CURVE ( 'NONE', #4249, #11970, #4401, .T. ) ;
#8605=CIRCLE ( 'NONE', #2298, 2.500000000000002220 ) ;
#8622=ORIENTED_EDGE ( 'NONE', *, *, #4123, .T. ) ;
#8627=CARTESIAN_POINT ( 'NONE',  ( 4.211399264691415567, -2.459727859270663952, -3.451161839612804094 ) ) ;
#8634=ORIENTED_EDGE ( 'NONE', *, *, #9945, .F. ) ;
#8654=CARTESIAN_POINT ( 'NONE',  ( 1.999999999999996225, 3.464101615137748613, -2.842992957459213432 ) ) ;
#8656=FACE_BOUND ( 'NONE', #3425, .T. ) ;
#8661=TOROIDAL_SURFACE ( 'NONE', #10537, 3.199999999999998845, 0.8000000000000001554 ) ;
#8684=ORIENTED_EDGE ( 'NONE', *, *, #8123, .F. ) ;
#8700=EDGE_LOOP ( 'NONE', ( #8389, #2439, #14333, #8442, #5140 ) ) ;
#8707=EDGE_CURVE ( 'NONE', #11445, #6869, #13285, .T. ) ;
#8721=CARTESIAN_POINT ( 'NONE',  ( 0.02511946470933534847, -4.877415451931371493, -3.451298686683617500 ) ) ;
#8724=DIRECTION ( 'NONE',  ( -1.000000000000000000, -4.406877377903812337E-17, 0.000000000000000000 ) ) ;
#8730=B_SPLINE_CURVE_WITH_KNOTS ( 'NONE', 3,
 ( #6013, #9024, #2384, #9247, #9320, #11370 ),
 .UNSPECIFIED., .F., .F.,
 ( 4, 2, 4 ),
 ( 0.003358874760055534110, 0.004541967308452078168, 0.005725059856848621793 ),
 .UNSPECIFIED. ) ;
#8736=CARTESIAN_POINT ( 'NONE',  ( 4.141042022537586575, -2.227970427079388305, -3.387027626239151878 ) ) ;
#8740=DIRECTION ( 'NONE',  ( 0.000000000000000000, 0.000000000000000000, 1.000000000000000000 ) ) ;
#8743=CARTESIAN_POINT ( 'NONE',  ( 4.211140560182194292, -2.431303136016548017, -3.445885042887453231 ) ) ;
#8747=LINE ( 'NONE', #988, #12357 ) ;
#8749=VERTEX_POINT ( 'NONE', #3723 ) ;
#8778=ADVANCED_FACE ( 'NONE', ( #6991 ), #8325, .F. ) ;
#8783=EDGE_LOOP ( 'NONE', ( #10305, #6672, #12083, #4013, #12857 ) ) ;
#8785=EDGE_CURVE ( 'NONE', #7559, #12838, #3015, .T. ) ;
#8806=DIRECTION ( 'NONE',  ( 0.000000000000000000, 0.000000000000000000, 1.000000000000000000 ) ) ;
#8814=CARTESIAN_POINT ( 'NONE',  ( -2.344047193898588510, -3.265465875126481787, -1.015423097168454931E-14 ) ) ;
#8830=AXIS2_PLACEMENT_3D ( 'NONE', #12631, #8167, #11539 ) ;
#8850=CARTESIAN_POINT ( 'NONE',  ( 0.6666666666666679619, -4.233901974057278750, -3.000726591567075552 ) ) ;
#8879=COLOUR_RGB ( '', 0.31764706, 0.68627451, 0.89019608) ;
#8883=SHAPE_REPRESENTATION ( 'torque nut 04-2_iso_ISO 7043-M5-N', ( #11025 ), #11250 ) ;
#8886=LINE ( 'NONE', #13166, #9118 ) ;
#8895=VERTEX_POINT ( 'NONE', #10670 ) ;
#8904=VECTOR ( 'NONE', #9135, 1000.000000000000000 ) ;
#8921=DIRECTION ( 'NONE',  ( 1.000000000000000000, 1.665334536937734071E-16, 0.000000000000000000 ) ) ;
#8923=DIRECTION ( 'NONE',  ( 1.000000000000000000, 1.665334536937734318E-16, 0.000000000000000000 ) ) ;
#8927=DIRECTION ( 'NONE',  ( 0.000000000000000000, 0.000000000000000000, 1.000000000000000000 ) ) ;
#8955=CARTESIAN_POINT ( 'NONE',  ( -3.349226789952651995, -2.685125164760746586, -0.2236248678334861184 ) ) ;
#8970=CONICAL_SURFACE ( 'NONE', #8025, 2.500000000000002220, 0.9599310885968781459 ) ;
#8993=CARTESIAN_POINT ( 'NONE',  ( 0.000000000000000000, 4.618802153517016507, -4.699999999999981526 ) ) ;
#9013=CARTESIAN_POINT ( 'NONE',  ( -4.000000000000001776, -1.762750951161524442E-16, 13.31572692736082786 ) ) ;
#9017=CARTESIAN_POINT ( 'NONE',  ( 0.000000000000000000, 0.000000000000000000, 1.599999999999990319 ) ) ;
#9024=CARTESIAN_POINT ( 'NONE',  ( -3.999999999999994671, -1.942223658245632256, -0.3516579909967634809 ) ) ;
#9036=ADVANCED_FACE ( 'NONE', ( #1900 ), #3084, .T. ) ;
#9052=EDGE_LOOP ( 'NONE', ( #5254, #13759, #3258, #585 ) ) ;
#9055=AXIS2_PLACEMENT_3D ( 'NONE', #5676, #11458, #4605 ) ;
#9081=CARTESIAN_POINT ( 'NONE',  ( 0.000000000000000000, 0.000000000000000000, 13.31572692736082786 ) ) ;
#9106=ORIENTED_EDGE ( 'NONE', *, *, #1992, .F. ) ;
#9118=VECTOR ( 'NONE', #4528, 1000.000000000000000 ) ;
#9121=ORIENTED_EDGE ( 'NONE', *, *, #11968, .F. ) ;
#9131=CARTESIAN_POINT ( 'NONE',  ( 2.345747346278098888, -3.264484291692517193, -0.01223254789874875237 ) ) ;
#9135=DIRECTION ( 'NONE',  ( 0.000000000000000000, 0.000000000000000000, 1.000000000000000000 ) ) ;
#9146=CARTESIAN_POINT ( 'NONE',  ( -2.000000000000001776, 3.464101615137757495, 0.000000000000000000 ) ) ;
#9155=CARTESIAN_POINT ( 'NONE',  ( -2.000000000000001776, 3.464101615137757495, 0.000000000000000000 ) ) ;
#9161=DIRECTION ( 'NONE',  ( 0.000000000000000000, 0.000000000000000000, 1.000000000000000000 ) ) ;
#9164=DIRECTION ( 'NONE',  ( -1.000000000000000000, -1.665334536937734071E-16, 0.000000000000000000 ) ) ;
#9166=EDGE_CURVE ( 'NONE', #7617, #11427, #5086, .T. ) ;
#9178=VECTOR ( 'NONE', #3634, 1000.000000000000000 ) ;
#9183=CARTESIAN_POINT ( 'NONE',  ( 2.344047193898593839, 3.265465875126470241, -5.393482291641755831E-15 ) ) ;
#9188=CARTESIAN_POINT ( 'NONE',  ( -4.211140560182201398, -2.431303136016548017, -3.445885042887453231 ) ) ;
#9205=DIRECTION ( 'NONE',  ( 0.000000000000000000, 0.000000000000000000, 1.000000000000000000 ) ) ;
#9208=DIRECTION ( 'NONE',  ( 0.000000000000000000, 0.000000000000000000, 1.000000000000000000 ) ) ;
#9212=EDGE_CURVE ( 'NONE', #3878, #14186, #13280, .T. ) ;
#9221=CARTESIAN_POINT ( 'NONE',  ( -2.855764796983338183, 2.970025579236424740, -0.09382832055446015118 ) ) ;
#9223=EDGE_CURVE ( 'NONE', #11164, #6869, #6952, .T. ) ;
#9245=CYLINDRICAL_SURFACE ( 'NONE', #263, 2.100000000000000977 ) ;
#9247=CARTESIAN_POINT ( 'NONE',  ( -3.999999999999995559, -0.7890432684750890990, -0.04868663549882130265 ) ) ;
#9258=CARTESIAN_POINT ( 'NONE',  ( -0.6666666666666671848, -4.233901974057272533, -3.000726591567075996 ) ) ;
#9266=DIRECTION ( 'NONE',  ( 1.000000000000000000, 1.665334536937734071E-16, 0.000000000000000000 ) ) ;
#9277=B_SPLINE_CURVE_WITH_KNOTS ( 'NONE', 3,
 ( #6266, #7368, #5317, #1750, #11843, #1817, #5179, #1966 ),
 .UNSPECIFIED., .F., .F.,
 ( 4, 2, 2, 4 ),
 ( 2.465131517015980755E-07, 0.001183067374689848478, 0.001774477805458921998, 0.002365888236227995517 ),
 .UNSPECIFIED. ) ;
#9278=CARTESIAN_POINT ( 'NONE',  ( 4.000000000000003553, -2.309401076758511806, -0.5000000000000004441 ) ) ;
#9284=DIRECTION ( 'NONE',  ( 1.000000000000000000, 1.665334536937734071E-16, 0.000000000000000000 ) ) ;
#9298=CARTESIAN_POINT ( 'NONE',  ( -3.999999999999996447, 2.309401076758494487, -0.5000000000000004441 ) ) ;
#9304=ORIENTED_EDGE ( 'NONE', *, *, #8566, .T. ) ;
#9307=VERTEX_POINT ( 'NONE', #9188 ) ;
#9320=CARTESIAN_POINT ( 'NONE',  ( -3.999999999999996447, -0.3979232138631241811, 1.502636448429128999E-15 ) ) ;
#9322=CARTESIAN_POINT ( 'NONE',  ( -3.999999999999996447, -3.469446951953614189E-15, 0.000000000000000000 ) ) ;
#9328=ORIENTED_EDGE ( 'NONE', *, *, #12817, .T. ) ;
#9344=CARTESIAN_POINT ( 'NONE',  ( -3.999999999999996447, 2.309401076758494487, -3.133295621305376422 ) ) ;
#9387=CARTESIAN_POINT ( 'NONE',  ( -1.393927851585480271, 4.043713361053534960, -3.226374918436821559 ) ) ;
#9388=CARTESIAN_POINT ( 'NONE',  ( -3.199999999999999289, -1.586475856045371110E-16, 2.400000000000013234 ) ) ;
#9411=ORIENTED_EDGE ( 'NONE', *, *, #1404, .F. ) ;
#9427=ORIENTED_EDGE ( 'NONE', *, *, #9166, .F. ) ;
#9433=CARTESIAN_POINT ( 'NONE',  ( -3.999999999999996447, -3.469446951953614189E-15, 0.000000000000000000 ) ) ;
#9440=CARTESIAN_POINT ( 'NONE',  ( 4.211140560182201398, 2.431303136016537358, -3.445885042887453231 ) ) ;
#9444=CIRCLE ( 'NONE', #4323, 0.7999999999999999334 ) ;
#9448=ORIENTED_EDGE ( 'NONE', *, *, #213, .F. ) ;
#9451=( BOUNDED_SURFACE ( )  B_SPLINE_SURFACE ( 3, 2, ( 
 ( #3220, #5404, #8627 ),
 ( #5331, #13110, #13183 ),
 ( #3156, #9941, #1082 ),
 ( #3374, #9794, #2262 ),
 ( #3088, #13401, #12214 ),
 ( #14271, #7515, #12003 ) ),
 .UNSPECIFIED., .F., .F., .F. ) 
 B_SPLINE_SURFACE_WITH_KNOTS ( ( 4, 2, 4 ),
 ( 3, 3 ),
 ( 0.02018219363417822834, 0.02264238182714343323, 0.02510257002010863811 ),
 ( 0.000000000000000000, 1.000000000000000000 ),
 .UNSPECIFIED. ) 
 GEOMETRIC_REPRESENTATION_ITEM ( )  RATIONAL_B_SPLINE_SURFACE ( (
 ( 1.000000000000000000, 0.8047781633350724606, 1.000000000000000000),
 ( 1.000000000000000000, 0.8123767859461576979, 1.000000000000000000),
 ( 1.000000000000000000, 0.8190657615682831461, 1.000000000000000000),
 ( 1.000000000000000000, 0.8192365618914937420, 1.000000000000000000),
 ( 1.000000000000000000, 0.8126137554627822501, 1.000000000000000000),
 ( 1.000000000000000000, 0.8047712275319380826, 1.000000000000000000) ) ) 
 REPRESENTATION_ITEM ( '' )  SURFACE ( )  );
#9457=CLOSED_SHELL ( 'NONE', ( #13774, #1499, #13333, #5937, #13718, #622, #5545, #10743, #11799, #12038, #12713, #5706, #986, #9036, #7599, #3335, #1021, #6905, #9505, #7858, #14159, #14025, #13824, #9913, #5128, #1543, #10620, #8778, #10280, #135, #14353, #14341, #8032, #1271, #1136, #8177, #9965, #10053, #3478 ) ) ;
#9463=CARTESIAN_POINT ( 'NONE',  ( 0.000000000000000000, 4.862606272033096033, -3.445885042887453231 ) ) ;
#9466=EDGE_LOOP ( 'NONE', ( #9951, #11293, #12306, #13016, #11211 ) ) ;
#9497=B_SPLINE_CURVE_WITH_KNOTS ( 'NONE', 3,
 ( #10232, #10309, #1302, #8099 ),
 .UNSPECIFIED., .F., .F.,
 ( 4, 4 ),
 ( 0.000000000000000000, 0.002452478801916362430 ),
 .UNSPECIFIED. ) ;
#9500=FACE_OUTER_BOUND ( 'NONE', #8454, .T. ) ;
#9503=CARTESIAN_POINT ( 'NONE',  ( 4.211140560182201398, 2.431303136016537358, -3.445885042887453231 ) ) ;
#9505=ADVANCED_FACE ( 'NONE', ( #3273 ), #891, .T. ) ;
#9522=B_SPLINE_CURVE_WITH_KNOTS ( 'NONE', 3,
 ( #9298, #8265, #12515, #9221, #10245, #3675, #1390, #9146 ),
 .UNSPECIFIED., .F., .F.,
 ( 4, 2, 2, 4 ),
 ( 2.465131517103448553E-07, 0.001183067374689843708, 0.001774477805458910071, 0.002365888236227976869 ),
 .UNSPECIFIED. ) ;
#9615=EDGE_LOOP ( 'NONE', ( #8684, #12110 ) ) ;
#9624=FACE_OUTER_BOUND ( 'NONE', #8151, .T. ) ;
#9625=AXIS2_PLACEMENT_3D ( 'NONE', #5555, #11124, #8923 ) ;
#9628=CARTESIAN_POINT ( 'NONE',  ( -3.861362476283257905, -2.629030857716000646, -3.371615880910393326 ) ) ;
#9650=EDGE_CURVE ( 'NONE', #13002, #7536, #6733, .T. ) ;
#9657=CARTESIAN_POINT ( 'NONE',  ( 0.000000000000000000, 4.618802153517016507, -3.133295621305376422 ) ) ;
#9665=B_SPLINE_CURVE_WITH_KNOTS ( 'NONE', 3,
 ( #11335, #10167, #13550, #85, #6799, #9131, #151, #7894 ),
 .UNSPECIFIED., .F., .F.,
 ( 4, 2, 2, 4 ),
 ( 2.465131517153036509E-07, 0.001183067374689848045, 0.001774477805458914408, 0.002365888236227980772 ),
 .UNSPECIFIED. ) ;
#9671=SURFACE_STYLE_USAGE ( .BOTH. , #4278 ) ;
#9676=CARTESIAN_POINT ( 'NONE',  ( 4.000000000000003553, 2.309401076758511806, -0.5000000000000004441 ) ) ;
#9742=CARTESIAN_POINT ( 'NONE',  ( 5.384454397937120440, 8.966917871450958727E-16, -4.699999999999981526 ) ) ;
#9746=CARTESIAN_POINT ( 'NONE',  ( 4.000000000000005329, 1.539600717839000099, -3.000726591567076440 ) ) ;
#9755=ORIENTED_EDGE ( 'NONE', *, *, #13227, .F. ) ;
#9756=CARTESIAN_POINT ( 'NONE',  ( 4.197393957002307552, 7.823395958202418729E-14, -3.203767560748914445 ) ) ;
#9770=CARTESIAN_POINT ( 'NONE',  ( -3.999999999999996447, 2.309401076758494487, -0.5000000000000004441 ) ) ;
#9781=B_SPLINE_CURVE_WITH_KNOTS ( 'NONE', 3,
 ( #11576, #10485, #467, #4922, #9387, #13870, #5004, #9463 ),
 .UNSPECIFIED., .F., .F.,
 ( 4, 2, 2, 4 ),
 ( 0.000000000000000000, 0.002450665683189815792, 0.003675998524784723689, 0.004901331366379631585 ),
 .UNSPECIFIED. ) ;
#9785=ORIENTED_EDGE ( 'NONE', *, *, #834, .T. ) ;
#9794=CARTESIAN_POINT ( 'NONE',  ( 3.999999999999998224, 0.8228621380349545600, -3.130611579770202546 ) ) ;
#9810=PRESENTATION_STYLE_ASSIGNMENT (( #9671 ) ) ;
#9815=ORIENTED_EDGE ( 'NONE', *, *, #14294, .T. ) ;
#9817=CARTESIAN_POINT ( 'NONE',  ( -0.6810530063607231899, -4.461079733297850680, -3.298443181296113025 ) ) ;
#9825=EDGE_LOOP ( 'NONE', ( #3413, #4051, #60, #7392 ) ) ;
#9840=CARTESIAN_POINT ( 'NONE',  ( 4.197393957002307552, 7.823395958202418729E-14, -3.203767560748914445 ) ) ;
#9844=DIRECTION ( 'NONE',  ( 0.000000000000000000, 0.000000000000000000, 1.000000000000000000 ) ) ;
#9845=CARTESIAN_POINT ( 'NONE',  ( -3.999999999999996447, 0.7924765000094545764, -0.05906175389889514044 ) ) ;
#9853=CARTESIAN_POINT ( 'NONE',  ( -4.000000000000000000, -2.309401076758511806, -3.133295621305376422 ) ) ;
#9905=FACE_OUTER_BOUND ( 'NONE', #2156, .T. ) ;
#9913=ADVANCED_FACE ( 'NONE', ( #12101 ), #5421, .T. ) ;
#9919=CARTESIAN_POINT ( 'NONE',  ( -3.510273485745311284, -2.827716139362665082, -3.310536846335872418 ) ) ;
#9925=( BOUNDED_SURFACE ( )  B_SPLINE_SURFACE ( 3, 2, ( 
 ( #8219, #13669, #2753 ),
 ( #1566, #5016, #12845 ),
 ( #7271, #10497, #8068 ),
 ( #12688, #4794, #1501 ),
 ( #6971, #6014, #7192 ),
 ( #7045, #7118, #10573 ) ),
 .UNSPECIFIED., .F., .F., .T. ) 
 B_SPLINE_SURFACE_WITH_KNOTS ( ( 4, 2, 4 ),
 ( 3, 3 ),
 ( 0.02023740217035200836, 0.02269762987400599299, 0.02515785757765997763 ),
 ( 0.000000000000000000, 1.000000000000000000 ),
 .UNSPECIFIED. ) 
 GEOMETRIC_REPRESENTATION_ITEM ( )  RATIONAL_B_SPLINE_SURFACE ( (
 ( 1.000000000000000000, 0.8047781539129733597, 1.000000000000000000),
 ( 1.000000000000000000, 0.8123770319057124212, 1.000000000000000000),
 ( 1.000000000000000000, 0.8190663783056869596, 1.000000000000000000),
 ( 1.000000000000000000, 0.8192359702877044514, 1.000000000000000000),
 ( 1.000000000000000000, 0.8126134888419825897, 1.000000000000000000),
 ( 1.000000000000000000, 0.8047712368238113534, 1.000000000000000000) ) ) 
 REPRESENTATION_ITEM ( '' )  SURFACE ( )  );
#9933=CARTESIAN_POINT ( 'NONE',  ( 0.000000000000000000, 0.000000000000000000, -4.699999999999981526 ) ) ;
#9941=CARTESIAN_POINT ( 'NONE',  ( 3.999999999999998224, -0.8577736050348424568, -3.133260139357294083 ) ) ;
#9944=DIRECTION ( 'NONE',  ( 0.000000000000000000, 0.000000000000000000, 1.000000000000000000 ) ) ;
#9945=EDGE_CURVE ( 'NONE', #8749, #2554, #14379, .T. ) ;
#9951=ORIENTED_EDGE ( 'NONE', *, *, #12936, .F. ) ;
#9965=ADVANCED_FACE ( 'NONE', ( #8656, #9905 ), #7694, .F. ) ;
#9987=FACE_BOUND ( 'NONE', #9615, .T. ) ;
#9995=DIRECTION ( 'NONE',  ( 1.000000000000000000, 1.665334536937733825E-16, 0.000000000000000000 ) ) ;
#10021=CARTESIAN_POINT ( 'NONE',  ( 0.000000000000000000, 0.000000000000000000, -4.184454397937131809 ) ) ;
#10024=CARTESIAN_POINT ( 'NONE',  ( 4.000000000000003553, -2.309401076758511806, -3.133295621305376422 ) ) ;
#10026=FACE_OUTER_BOUND ( 'NONE', #13040, .T. ) ;
#10046=CARTESIAN_POINT ( 'NONE',  ( 2.000000000000015543, 3.464101615137753942, 0.000000000000000000 ) ) ;
#10053=ADVANCED_FACE ( 'NONE', ( #11075 ), #12434, .T. ) ;
#10055=DIRECTION ( 'NONE',  ( -1.000000000000000000, -4.406877377903811104E-17, 0.000000000000000000 ) ) ;
#10091=ORIENTED_EDGE ( 'NONE', *, *, #13533, .F. ) ;
#10098=DIRECTION ( 'NONE',  ( -0.8660254037844381525, -0.5000000000000008882, 0.000000000000000000 ) ) ;
#10102=VECTOR ( 'NONE', #2422, 1000.000000000000000 ) ;
#10125=EDGE_CURVE ( 'NONE', #1916, #4911, #2885, .T. ) ;
#10129=PRODUCT_DEFINITION_FORMATION_WITH_SPECIFIED_SOURCE ( 'ANY', '', #3937, .NOT_KNOWN. ) ;
#10153=DIRECTION ( 'NONE',  ( 0.000000000000000000, 0.000000000000000000, 1.000000000000000000 ) ) ;
#10162=CARTESIAN_POINT ( 'NONE',  ( -2.725758460534058791, 3.045084772581766686, -2.920601398289325079 ) ) ;
#10165=CARTESIAN_POINT ( 'NONE',  ( 0.000000000000000000, 0.000000000000000000, -4.184454397937131809 ) ) ;
#10167=CARTESIAN_POINT ( 'NONE',  ( 3.680118525130247065, -2.494084732383348602, -0.3507732604232590701 ) ) ;
#10171=EDGE_CURVE ( 'NONE', #10589, #12756, #2181, .T. ) ;
#10172=CARTESIAN_POINT ( 'NONE',  ( -4.000000000000000000, -1.762750951161524442E-16, 1.599999999999990319 ) ) ;
#10173=ORIENTED_EDGE ( 'NONE', *, *, #299, .T. ) ;
#10188=DIRECTION ( 'NONE',  ( -4.406877377903809255E-17, 1.000000000000000000, 0.000000000000000000 ) ) ;
#10221=CARTESIAN_POINT ( 'NONE',  ( -3.999999999999991118, 2.471529427528112777, -3.386887593711393585 ) ) ;
#10223=AXIS2_PLACEMENT_3D ( 'NONE', #7946, #276, #13463 ) ;
#10232=CARTESIAN_POINT ( 'NONE',  ( 4.211140560182201398, 2.431303136016537358, -3.445885042887453231 ) ) ;
#10245=CARTESIAN_POINT ( 'NONE',  ( -2.687328764639631551, 3.067272167851298192, -0.05923475698270941336 ) ) ;
#10250=CARTESIAN_POINT ( 'NONE',  ( 3.000000000000001332, 4.996003610813205418E-16, 2.400000000000013234 ) ) ;
#10257=EDGE_CURVE ( 'NONE', #13588, #7727, #13355, .T. ) ;
#10259=CARTESIAN_POINT ( 'NONE',  ( -3.200000000000000178, -1.410200760929219011E-16, 1.599999999999990319 ) ) ;
#10280=ADVANCED_FACE ( 'NONE', ( #4473 ), #9451, .F. ) ;
#10282=FACE_OUTER_BOUND ( 'NONE', #7373, .T. ) ;
#10290=B_SPLINE_CURVE_WITH_KNOTS ( 'NONE', 3,
 ( #8509, #5431, #7333, #9746, #11883 ),
 .UNSPECIFIED., .F., .F.,
 ( 4, 1, 4 ),
 ( 0.000000000000000000, 0.002309401076758504923, 0.004618802153517009845 ),
 .UNSPECIFIED. ) ;
#10291=CARTESIAN_POINT ( 'NONE',  ( -4.211405941597120339, -2.460460478483087243, -3.451298436431144978 ) ) ;
#10305=ORIENTED_EDGE ( 'NONE', *, *, #13636, .T. ) ;
#10309=CARTESIAN_POINT ( 'NONE',  ( 4.203833317240883716, 1.627343821129582535, -3.297273115243909203 ) ) ;
#10320=DIRECTION ( 'NONE',  ( 1.000000000000000000, 1.665334536937734071E-16, 0.000000000000000000 ) ) ;
#10342=CARTESIAN_POINT ( 'NONE',  ( -2.000000000000001776, 3.464101615137757495, 0.000000000000000000 ) ) ;
#10345=DIRECTION ( 'NONE',  ( 0.000000000000000000, 0.000000000000000000, -1.000000000000000000 ) ) ;
#10351=DIRECTION ( 'NONE',  ( 0.000000000000000000, 0.000000000000000000, 1.000000000000000000 ) ) ;
#10362=CARTESIAN_POINT ( 'NONE',  ( -3.999999999999996447, 2.309401076758494487, -0.5000000000000004441 ) ) ;
#10374=CARTESIAN_POINT ( 'NONE',  ( -3.999999999999991562, 1.700072946616246972, -3.020308295356175066 ) ) ;
#10377=AXIS2_PLACEMENT_3D ( 'NONE', #3984, #391, #1630 ) ;
#10379=ORIENTED_EDGE ( 'NONE', *, *, #1117, .F. ) ;
#10391=CARTESIAN_POINT ( 'NONE',  ( 0.3208286057739703212, -4.433571671609695564, -0.3503314178412707536 ) ) ;
#10393=EDGE_CURVE ( 'NONE', #12838, #14315, #3761, .T. ) ;
#10402=EDGE_CURVE ( 'NONE', #12541, #13711, #8085, .T. ) ;
#10422=ORIENTED_EDGE ( 'NONE', *, *, #7179, .F. ) ;
#10427=DIRECTION ( 'NONE',  ( 0.000000000000000000, 0.000000000000000000, 1.000000000000000000 ) ) ;
#10436=CARTESIAN_POINT ( 'NONE',  ( -3.999999999999991562, -0.8382426107201307319, -2.920612530944965979 ) ) ;
#10439=CYLINDRICAL_SURFACE ( 'NONE', #8830, 2.500000000000002220 ) ;
#10441=CARTESIAN_POINT ( 'NONE',  ( 0.000000000000000000, 0.000000000000000000, 1.599999999999990319 ) ) ;
#10455=DIRECTION ( 'NONE',  ( 0.000000000000000000, 0.000000000000000000, 1.000000000000000000 ) ) ;
#10465=ORIENTED_EDGE ( 'NONE', *, *, #2932, .F. ) ;
#10485=CARTESIAN_POINT ( 'NONE',  ( -3.511755186886741154, 2.826662030176364304, -3.297382984111596915 ) ) ;
#10497=CARTESIAN_POINT ( 'NONE',  ( 2.742797192660133998, 3.035247456002194255, -3.133250573521593640 ) ) ;
#10515=FILL_AREA_STYLE_COLOUR ( '', #8879 ) ;
#10518=CARTESIAN_POINT ( 'NONE',  ( -3.999999999999991562, 0.8730390046630041034, -2.923132639555956480 ) ) ;
#10528=CARTESIAN_POINT ( 'NONE',  ( -1.312671235360381994, -3.860931062424226567, -0.05923475698271308404 ) ) ;
#10537=AXIS2_PLACEMENT_3D ( 'NONE', #2916, #5499, #12939 ) ;
#10538=LINE ( 'NONE', #8040, #8904 ) ;
#10542=VERTEX_POINT ( 'NONE', #3941 ) ;
#10573=CARTESIAN_POINT ( 'NONE',  ( -0.02511946470933182005, 4.877415451931357282, -3.451298686683612171 ) ) ;
#10576=CARTESIAN_POINT ( 'NONE',  ( 0.000000000000000000, 0.000000000000000000, 1.599999999999990319 ) ) ;
#10581=ORIENTED_EDGE ( 'NONE', *, *, #1775, .T. ) ;
#10589=VERTEX_POINT ( 'NONE', #10595 ) ;
#10595=CARTESIAN_POINT ( 'NONE',  ( -4.197393957002300446, -7.772664289393031077E-14, -3.203767560748911780 ) ) ;
#10606=CARTESIAN_POINT ( 'NONE',  ( -1.387778780781445676E-14, -4.618802153517016507, -0.5000000000000004441 ) ) ;
#10620=ADVANCED_FACE ( 'NONE', ( #1945 ), #1316, .F. ) ;
#10630=CARTESIAN_POINT ( 'NONE',  ( 4.000000000000003553, 0.000000000000000000, 0.000000000000000000 ) ) ;
#10636=CONICAL_SURFACE ( 'NONE', #360, 4.000000000000000000, 0.8911886515913775009 ) ;
#10653=CARTESIAN_POINT ( 'NONE',  ( 0.000000000000000000, -4.862606272033103139, -3.445885042887453231 ) ) ;
#10664=EDGE_LOOP ( 'NONE', ( #14180, #3730, #6474, #5951 ) ) ;
#10670=CARTESIAN_POINT ( 'NONE',  ( 4.000000000000003553, 0.000000000000000000, 0.000000000000000000 ) ) ;
#10675=DIRECTION ( 'NONE',  ( 1.000000000000000000, 1.665334536937734318E-16, 0.000000000000000000 ) ) ;
#10677=CARTESIAN_POINT ( 'NONE',  ( 0.000000000000000000, 0.000000000000000000, -3.699999999999981082 ) ) ;
#10688=CIRCLE ( 'NONE', #4393, 0.5155456020628804703 ) ;
#10695=CARTESIAN_POINT ( 'NONE',  ( -2.100000000000000977, -9.254442493598004305E-17, -4.699999999999981526 ) ) ;
#10708=B_SPLINE_CURVE_WITH_KNOTS ( 'NONE', 3,
 ( #10606, #3138, #3956, #8250, #10528, #2708, #13978, #8397 ),
 .UNSPECIFIED., .F., .F.,
 ( 4, 2, 2, 4 ),
 ( 2.465131517300305892E-07, 0.001183067374689865392, 0.001774477805458931972, 0.002365888236227998986 ),
 .UNSPECIFIED. ) ;
#10721=CARTESIAN_POINT ( 'NONE',  ( 2.712778981738061201, -3.052578478158764597, -3.130620751971683990 ) ) ;
#10729=CARTESIAN_POINT ( 'NONE',  ( -2.449848172108558764, -3.432307619358754724, -3.203702292528892048 ) ) ;
#10743=ADVANCED_FACE ( 'NONE', ( #11121 ), #14090, .T. ) ;
#10755=CARTESIAN_POINT ( 'NONE',  ( 2.804994570502175044, 3.229033611042453344, -3.226374918436819339 ) ) ;
#10769=EDGE_CURVE ( 'NONE', #2847, #6911, #9665, .T. ) ;
#10773=VECTOR ( 'NONE', #11537, 1000.000000000000114 ) ;
#10775=CARTESIAN_POINT ( 'NONE',  ( 4.000000000000002665, 1.941961291383483390, -0.3515519931180288160 ) ) ;
#10812=AXIS2_PLACEMENT_3D ( 'NONE', #738, #6361, #12806 ) ;
#10819=AXIS2_PLACEMENT_3D ( 'NONE', #11425, #2582, #3684 ) ;
#10844=CARTESIAN_POINT ( 'NONE',  ( 4.000000000000003553, 0.1981133338132486654, -4.511085718839590031E-15 ) ) ;
#10845=DIRECTION ( 'NONE',  ( 0.000000000000000000, 0.000000000000000000, -1.000000000000000000 ) ) ;
#10861=CARTESIAN_POINT ( 'NONE',  ( 2.725758460532844207, -3.045084772582480781, -2.920601398289143891 ) ) ;
#10864=CYLINDRICAL_SURFACE ( 'NONE', #8488, 2.500000000000002220 ) ;
#10906=CARTESIAN_POINT ( 'NONE',  ( 4.000000000000004441, 0.3987449864459970406, -0.01220643443060221052 ) ) ;
#10912=CARTESIAN_POINT ( 'NONE',  ( -2.756166666307275914, -3.027528586793036602, -2.923144239647422538 ) ) ;
#10920=CARTESIAN_POINT ( 'NONE',  ( 0.000000000000000000, 3.000000000000002665, 2.400000000000013234 ) ) ;
#10924=CARTESIAN_POINT ( 'NONE',  ( 3.455075492488635991, -2.624013387858225244, -3.016622336522302383 ) ) ;
#10938=CARTESIAN_POINT ( 'NONE',  ( -3.999999999999996447, 0.3987449864459917670, -0.01220643443059570010 ) ) ;
#10948=DIRECTION ( 'NONE',  ( 1.000000000000000000, 1.665334536937734318E-16, 0.000000000000000000 ) ) ;
#10955=AXIS2_PLACEMENT_3D ( 'NONE', #10165, #2126, #13547 ) ;
#11020=ORIENTED_EDGE ( 'NONE', *, *, #1117, .T. ) ;
#11023=( BOUNDED_SURFACE ( )  B_SPLINE_SURFACE ( 3, 2, ( 
 ( #3246, #4287, #11065 ),
 ( #3176, #3325, #6437 ),
 ( #10912, #7834, #7768 ),
 ( #7684, #5354, #12243 ),
 ( #4354, #13270, #9817 ),
 ( #14293, #4502, #8721 ) ),
 .UNSPECIFIED., .F., .F., .T. ) 
 B_SPLINE_SURFACE_WITH_KNOTS ( ( 4, 2, 4 ),
 ( 3, 3 ),
 ( 0.02023740217035201530, 0.02269762987400599993, 0.02515785757765998457 ),
 ( 0.000000000000000000, 1.000000000000000000 ),
 .UNSPECIFIED. ) 
 GEOMETRIC_REPRESENTATION_ITEM ( )  RATIONAL_B_SPLINE_SURFACE ( (
 ( 1.000000000000000000, 0.8047781539129736927, 1.000000000000000000),
 ( 1.000000000000000000, 0.8123770319057125322, 1.000000000000000000),
 ( 1.000000000000000000, 0.8190663783056868485, 1.000000000000000000),
 ( 1.000000000000000000, 0.8192359702877043404, 1.000000000000000000),
 ( 1.000000000000000000, 0.8126134888419832558, 1.000000000000000000),
 ( 1.000000000000000000, 0.8047712368238106873, 1.000000000000000000) ) ) 
 REPRESENTATION_ITEM ( '' )  SURFACE ( )  );
#11025=AXIS2_PLACEMENT_3D ( 'NONE', #167, #6524, #5441 ) ;
#11036=CARTESIAN_POINT ( 'NONE',  ( 4.000000000000003553, -2.309401076758511806, -3.133295621305376422 ) ) ;
#11055=CARTESIAN_POINT ( 'NONE',  ( 0.000000000000000000, -4.618802153517030717, -3.133295621305376422 ) ) ;
#11065=CARTESIAN_POINT ( 'NONE',  ( -4.235887314095728051, -2.417314327725976320, -3.451162025751973061 ) ) ;
#11071=CARTESIAN_POINT ( 'NONE',  ( -5.384454397937120440, -2.372863027862376680E-16, -4.184454397937131809 ) ) ;
#11075=FACE_OUTER_BOUND ( 'NONE', #7355, .T. ) ;
#11102=EDGE_LOOP ( 'NONE', ( #555, #9815, #12172, #11020, #7889 ) ) ;
#11110=EDGE_CURVE ( 'NONE', #8749, #12541, #12890, .T. ) ;
#11121=FACE_OUTER_BOUND ( 'NONE', #4817, .T. ) ;
#11124=DIRECTION ( 'NONE',  ( 0.000000000000000000, 0.000000000000000000, 1.000000000000000000 ) ) ;
#11133=FACE_OUTER_BOUND ( 'NONE', #7695, .T. ) ;
#11136=DIRECTION ( 'NONE',  ( 0.000000000000000000, 0.000000000000000000, 1.000000000000000000 ) ) ;
#11164=VERTEX_POINT ( 'NONE', #4973 ) ;
#11183=CARTESIAN_POINT ( 'NONE',  ( 4.000000000000003553, -1.942223658245632700, -0.3516579909967693096 ) ) ;
#11199=CARTESIAN_POINT ( 'NONE',  ( 1.069120652742303742E-15, 4.736522675502173207, -3.381124513963619904 ) ) ;
#11202=VERTEX_POINT ( 'NONE', #5329 ) ;
#11211=ORIENTED_EDGE ( 'NONE', *, *, #13248, .T. ) ;
#11217=VERTEX_POINT ( 'NONE', #9657 ) ;
#11218=B_SPLINE_CURVE_WITH_KNOTS ( 'NONE', 3,
 ( #13784, #1265, #2366, #12665 ),
 .UNSPECIFIED., .F., .F.,
 ( 4, 4 ),
 ( 0.000000000000000000, 0.002452478801916370670 ),
 .UNSPECIFIED. ) ;
#11250=( GEOMETRIC_REPRESENTATION_CONTEXT ( 3 ) GLOBAL_UNCERTAINTY_ASSIGNED_CONTEXT ( ( #621 ) ) GLOBAL_UNIT_ASSIGNED_CONTEXT ( ( #3972, #7094, #2576 ) ) REPRESENTATION_CONTEXT ( 'NONE', 'WORKASPACE' ) );
#11293=ORIENTED_EDGE ( 'NONE', *, *, #194, .F. ) ;
#11304=CARTESIAN_POINT ( 'NONE',  ( 0.000000000000000000, -4.618802153517030717, -3.133295621305376422 ) ) ;
#11310=CARTESIAN_POINT ( 'NONE',  ( 0.000000000000000000, 0.000000000000000000, 1.599999999999990319 ) ) ;
#11318=DIRECTION ( 'NONE',  ( 0.5000000000000014433, 0.8660254037844378194, 0.000000000000000000 ) ) ;
#11335=CARTESIAN_POINT ( 'NONE',  ( 4.000000000000003553, -2.309401076758511806, -0.5000000000000004441 ) ) ;
#11337=CARTESIAN_POINT ( 'NONE',  ( 0.000000000000000000, 0.000000000000000000, 1.159999999999994369 ) ) ;
#11355=ORIENTED_EDGE ( 'NONE', *, *, #13922, .T. ) ;
#11369=ORIENTED_EDGE ( 'NONE', *, *, #8052, .F. ) ;
#11370=CARTESIAN_POINT ( 'NONE',  ( -3.999999999999996447, -3.469446951953614189E-15, 0.000000000000000000 ) ) ;
#11380=DIRECTION ( 'NONE',  ( -0.8660254037844378194, 0.5000000000000014433, -0.000000000000000000 ) ) ;
#11425=CARTESIAN_POINT ( 'NONE',  ( 0.000000000000000000, 0.000000000000000000, -3.699999999999981082 ) ) ;
#11427=VERTEX_POINT ( 'NONE', #5677 ) ;
#11445=VERTEX_POINT ( 'NONE', #7652 ) ;
#11446=LINE ( 'NONE', #2834, #5169 ) ;
#11447=ORIENTED_EDGE ( 'NONE', *, *, #10393, .T. ) ;
#11458=DIRECTION ( 'NONE',  ( 0.000000000000000000, 0.000000000000000000, 1.000000000000000000 ) ) ;
#11462=CARTESIAN_POINT ( 'NONE',  ( -3.999999999999990674, -2.512220432843131235, -3.169390650195370807 ) ) ;
#11474=CARTESIAN_POINT ( 'NONE',  ( 0.000000000000000000, 0.000000000000000000, -4.394516984716101859 ) ) ;
#11492=AXIS2_PLACEMENT_3D ( 'NONE', #7765, #4571, #13263 ) ;
#11507=CARTESIAN_POINT ( 'NONE',  ( 6.938893903907228378E-15, 2.540000000000007585, 1.599999999999990319 ) ) ;
#11530=FACE_OUTER_BOUND ( 'NONE', #8700, .T. ) ;
#11537=DIRECTION ( 'NONE',  ( -0.7071067811865490160, -3.116132877773382125E-17, 0.7071067811865460184 ) ) ;
#11539=DIRECTION ( 'NONE',  ( 1.000000000000000000, 1.665334536937734071E-16, 0.000000000000000000 ) ) ;
#11544=VERTEX_POINT ( 'NONE', #2401 ) ;
#11545=DIRECTION ( 'NONE',  ( 0.000000000000000000, 0.000000000000000000, 1.000000000000000000 ) ) ;
#11560=CARTESIAN_POINT ( 'NONE',  ( 2.000000000000001776, -3.464101615137764156, 0.000000000000000000 ) ) ;
#11576=CARTESIAN_POINT ( 'NONE',  ( -4.211140560182194292, 2.431303136016534250, -3.445885042887453231 ) ) ;
#11581=MANIFOLD_SOLID_BREP ( 'TorqueElement', #9457 ) ;
#11588=LINE ( 'NONE', #5943, #9178 ) ;
#11606=SURFACE_STYLE_FILL_AREA ( #7134 ) ;
#11616=CARTESIAN_POINT ( 'NONE',  ( 4.000000000000003553, 0.000000000000000000, 0.000000000000000000 ) ) ;
#11627=CARTESIAN_POINT ( 'NONE',  ( -4.197393957002299558, 0.4069871074557444568, -3.203767560748908227 ) ) ;
#11637=CARTESIAN_POINT ( 'NONE',  ( -4.154094228333754302, -2.398367420967508767, -3.421909803043237996 ) ) ;
#11649=DIRECTION ( 'NONE',  ( 0.000000000000000000, 0.000000000000000000, 1.000000000000000000 ) ) ;
#11652=FACE_OUTER_BOUND ( 'NONE', #220, .T. ) ;
#11667=ORIENTED_EDGE ( 'NONE', *, *, #1992, .T. ) ;
#11672=EDGE_CURVE ( 'NONE', #7122, #13364, #8886, .T. ) ;
#11722=MECHANICAL_DESIGN_GEOMETRIC_PRESENTATION_REPRESENTATION('',(#3555),#13142);
#11728=B_SPLINE_CURVE_WITH_KNOTS ( 'NONE', 3,
 ( #982, #8594, #5447, #10729, #12184, #9919, #9628, #11905 ),
 .UNSPECIFIED., .F., .F.,
 ( 4, 2, 2, 4 ),
 ( 0.000000000000000000, 0.002450665683189818828, 0.003675998524784728459, 0.004901331366379637657 ),
 .UNSPECIFIED. ) ;
#11734=VECTOR ( 'NONE', #5291, 1000.000000000000114 ) ;
#11752=B_SPLINE_CURVE_WITH_KNOTS ( 'NONE', 3,
 ( #4213, #893, #8654, #13144, #6238 ),
 .UNSPECIFIED., .F., .F.,
 ( 4, 1, 4 ),
 ( 0.000000000000000000, 0.002309401076758504923, 0.004618802153517009845 ),
 .UNSPECIFIED. ) ;
#11753=CARTESIAN_POINT ( 'NONE',  ( -3.999999999999996447, 1.539600717838993882, -3.000726591567075108 ) ) ;
#11779=EDGE_LOOP ( 'NONE', ( #12405, #8118, #9304, #12204 ) ) ;
#11786=SHAPE_DEFINITION_REPRESENTATION ( #12805, #8883 ) ;
#11792=DIRECTION ( 'NONE',  ( 0.000000000000000000, 0.000000000000000000, 1.000000000000000000 ) ) ;
#11799=ADVANCED_FACE ( 'NONE', ( #330 ), #9245, .F. ) ;
#11806=CARTESIAN_POINT ( 'NONE',  ( 0.000000000000000000, 0.000000000000000000, 0.000000000000000000 ) ) ;
#11827=DIRECTION ( 'NONE',  ( 1.665334536937734071E-16, -1.000000000000000000, 0.000000000000000000 ) ) ;
#11843=CARTESIAN_POINT ( 'NONE',  ( 1.312671235360379107, 3.860931062424219462, -0.05923475698270710271 ) ) ;
#11856=PRODUCT_CONTEXT ( 'NONE', #14381, 'mechanical' ) ;
#11873=ORIENTED_EDGE ( 'NONE', *, *, #7659, .T. ) ;
#11881=PRODUCT_DEFINITION ( 'UNKNOWN', '', #10129, #6438 ) ;
#11883=CARTESIAN_POINT ( 'NONE',  ( 4.000000000000003553, 2.309401076758501592, -3.133295621305376422 ) ) ;
#11900=CARTESIAN_POINT ( 'NONE',  ( 1.393927851585489375, -4.043713361053542954, -3.226374918436825112 ) ) ;
#11905=CARTESIAN_POINT ( 'NONE',  ( -4.211140560182201398, -2.431303136016548017, -3.445885042887453231 ) ) ;
#11921=ORIENTED_EDGE ( 'NONE', *, *, #3513, .F. ) ;
#11934=CYLINDRICAL_SURFACE ( 'NONE', #2395, 3.000000000000001332 ) ;
#11940=AXIS2_PLACEMENT_3D ( 'NONE', #9017, #9844, #5520 ) ;
#11942=CARTESIAN_POINT ( 'NONE',  ( -4.000000000000000000, -2.309401076758511806, -3.204269196027522693 ) ) ;
#11950=DIRECTION ( 'NONE',  ( 0.000000000000000000, 0.000000000000000000, -1.000000000000000000 ) ) ;
#11968=EDGE_CURVE ( 'NONE', #12756, #698, #5319, .T. ) ;
#11970=VERTEX_POINT ( 'NONE', #10172 ) ;
#11971=CARTESIAN_POINT ( 'NONE',  ( 2.805705207896079578, -3.226868319750171743, -3.203898532754354544 ) ) ;
#11973=CARTESIAN_POINT ( 'NONE',  ( -2.540000000000002700, -1.119346853987568578E-16, 1.599999999999990319 ) ) ;
#11985=CIRCLE ( 'NONE', #11492, 4.000000000000000000 ) ;
#12003=CARTESIAN_POINT ( 'NONE',  ( 4.211405962802040825, 2.460462805100875450, -3.451298870276212405 ) ) ;
#12008=EDGE_CURVE ( 'NONE', #12541, #8749, #13611, .T. ) ;
#12009=ORIENTED_EDGE ( 'NONE', *, *, #13910, .T. ) ;
#12037=PLANE ( 'NONE',  #5762 ) ;
#12038=ADVANCED_FACE ( 'NONE', ( #10026 ), #13421, .F. ) ;
#12039=CARTESIAN_POINT ( 'NONE',  ( 2.807096675499392902, -3.225959780909705366, -3.202509183706237827 ) ) ;
#12083=ORIENTED_EDGE ( 'NONE', *, *, #7179, .T. ) ;
#12087=CIRCLE ( 'NONE', #13967, 2.500000000000002220 ) ;
#12101=FACE_OUTER_BOUND ( 'NONE', #12638, .T. ) ;
#12110=ORIENTED_EDGE ( 'NONE', *, *, #382, .F. ) ;
#12116=DIRECTION ( 'NONE',  ( 1.000000000000000000, 1.665334536937734071E-16, 0.000000000000000000 ) ) ;
#12122=EDGE_CURVE ( 'NONE', #10542, #7617, #10538, .T. ) ;
#12123=ORIENTED_EDGE ( 'NONE', *, *, #9650, .T. ) ;
#12141=EDGE_CURVE ( 'NONE', #6911, #6532, #67, .T. ) ;
#12155=( LENGTH_UNIT ( ) NAMED_UNIT ( * ) SI_UNIT ( .MILLI., .METRE. ) );
#12156=DIRECTION ( 'NONE',  ( 1.000000000000000000, 1.665334536937734318E-16, 0.000000000000000000 ) ) ;
#12172=ORIENTED_EDGE ( 'NONE', *, *, #4198, .T. ) ;
#12179=FACE_OUTER_BOUND ( 'NONE', #14038, .T. ) ;
#12184=CARTESIAN_POINT ( 'NONE',  ( -2.804994570502171047, -3.229033611042463114, -3.226374918436821115 ) ) ;
#12204=ORIENTED_EDGE ( 'NONE', *, *, #2932, .T. ) ;
#12211=DIRECTION ( 'NONE',  ( 0.8660254037844380415, 0.5000000000000009992, 0.000000000000000000 ) ) ;
#12214=CARTESIAN_POINT ( 'NONE',  ( 4.203935404774708395, 1.640788256319067662, -3.298453876328925283 ) ) ;
#12225=ORIENTED_EDGE ( 'NONE', *, *, #4645, .T. ) ;
#12235=CARTESIAN_POINT ( 'NONE',  ( -4.211140560182194292, 2.431303136016534250, -3.445885042887453231 ) ) ;
#12236=ORIENTED_EDGE ( 'NONE', *, *, #10402, .T. ) ;
#12243=CARTESIAN_POINT ( 'NONE',  ( -1.390214784104929269, -4.043996922316123843, -3.202509183706211182 ) ) ;
#12257=DIRECTION ( 'NONE',  ( -1.000000000000000000, -1.665334536937734071E-16, 0.000000000000000000 ) ) ;
#12258=VERTEX_POINT ( 'NONE', #3668 ) ;
#12263=CARTESIAN_POINT ( 'NONE',  ( -2.000000000000001776, -3.464101615137750390, 0.000000000000000000 ) ) ;
#12293=CARTESIAN_POINT ( 'NONE',  ( 0.1404055950190679636, 4.699865361596996749, -3.386887224136954533 ) ) ;
#12306=ORIENTED_EDGE ( 'NONE', *, *, #7835, .F. ) ;
#12308=CARTESIAN_POINT ( 'NONE',  ( 4.000000000000003553, 2.309401076758511806, -0.5000000000000004441 ) ) ;
#12342=AXIS2_PLACEMENT_3D ( 'NONE', #8306, #6921, #9266 ) ;
#12350=AXIS2_PLACEMENT_3D ( 'NONE', #3145, #14189, #10948 ) ;
#12357=VECTOR ( 'NONE', #7631, 1000.000000000000000 ) ;
#12393=DIRECTION ( 'NONE',  ( 0.000000000000000000, 0.000000000000000000, -1.000000000000000000 ) ) ;
#12405=ORIENTED_EDGE ( 'NONE', *, *, #2623, .F. ) ;
#12421=DIRECTION ( 'NONE',  ( 0.000000000000000000, 0.000000000000000000, 1.000000000000000000 ) ) ;
#12434=TOROIDAL_SURFACE ( 'NONE', #1924, 3.199999999999998845, 0.8000000000000001554 ) ;
#12436=FACE_OUTER_BOUND ( 'NONE', #7563, .T. ) ;
#12451=LINE ( 'NONE', #5828, #10102 ) ;
#12461=CONICAL_SURFACE ( 'NONE', #6612, 4.000000000000000000, 0.8911886515913775009 ) ;
#12462=CARTESIAN_POINT ( 'NONE',  ( -5.560781378645576645, -9.260561282218706512E-16, -3.699999999999981082 ) ) ;
#12477=CARTESIAN_POINT ( 'NONE',  ( 0.000000000000000000, 0.000000000000000000, -4.699999999999981526 ) ) ;
#12481=ORIENTED_EDGE ( 'NONE', *, *, #8159, .F. ) ;
#12496=DIRECTION ( 'NONE',  ( 1.000000000000000000, 1.665334536937734071E-16, 0.000000000000000000 ) ) ;
#12503=CARTESIAN_POINT ( 'NONE',  ( -0.5469803261939266692, 4.303002914946603141, -3.235259548912158944 ) ) ;
#12515=CARTESIAN_POINT ( 'NONE',  ( -3.355112389629170355, 2.681727112203163621, -0.2256878752776750874 ) ) ;
#12537=ORIENTED_EDGE ( 'NONE', *, *, #8079, .F. ) ;
#12541=VERTEX_POINT ( 'NONE', #3803 ) ;
#12553=DIRECTION ( 'NONE',  ( 0.000000000000000000, 0.000000000000000000, 1.000000000000000000 ) ) ;
#12600=B_SPLINE_CURVE_WITH_KNOTS ( 'NONE', 3,
 ( #9278, #11183, #1162, #12717, #7219, #11616 ),
 .UNSPECIFIED., .F., .F.,
 ( 4, 2, 4 ),
 ( 0.003358874760055545385, 0.004541967308452085975, 0.005725059856848626130 ),
 .UNSPECIFIED. ) ;
#12607=DIRECTION ( 'NONE',  ( 1.000000000000000000, 1.665334536937734071E-16, 0.000000000000000000 ) ) ;
#12631=CARTESIAN_POINT ( 'NONE',  ( 0.000000000000000000, 0.000000000000000000, -25.03750572909319061 ) ) ;
#12638=EDGE_LOOP ( 'NONE', ( #3234, #12481, #10379 ) ) ;
#12643=DIRECTION ( 'NONE',  ( 0.000000000000000000, 0.000000000000000000, 1.000000000000000000 ) ) ;
#12652=CIRCLE ( 'NONE', #9625, 3.000000000000001332 ) ;
#12665=CARTESIAN_POINT ( 'NONE',  ( -4.197393957002300446, -7.772664289393031077E-14, -3.203767560748911780 ) ) ;
#12682=EDGE_CURVE ( 'NONE', #2216, #13588, #7199, .T. ) ;
#12688=CARTESIAN_POINT ( 'NONE',  ( 1.274241539467095841, 3.883118457693076397, -2.920601398289139006 ) ) ;
#12712=CARTESIAN_POINT ( 'NONE',  ( 0.000000000000000000, 4.618802153517016507, -3.133295621305376422 ) ) ;
#12713=ADVANCED_FACE ( 'NONE', ( #153 ), #4621, .T. ) ;
#12717=CARTESIAN_POINT ( 'NONE',  ( 4.000000000000004441, -0.7890432684750890990, -0.04868663549882738112 ) ) ;
#12721=ORIENTED_EDGE ( 'NONE', *, *, #2187, .F. ) ;
#12725=CARTESIAN_POINT ( 'NONE',  ( -1.387778780781445676E-14, -4.618802153517016507, -0.5000000000000004441 ) ) ;
#12742=CARTESIAN_POINT ( 'NONE',  ( 4.211140560182194292, -2.431303136016548017, -3.445885042887453231 ) ) ;
#12743=EDGE_CURVE ( 'NONE', #11427, #7617, #12652, .T. ) ;
#12750=CARTESIAN_POINT ( 'NONE',  ( -1.317756351988340180, 3.857995168970207889, -0.04852650426602111294 ) ) ;
#12756=VERTEX_POINT ( 'NONE', #3389 ) ;
#12764=FACE_OUTER_BOUND ( 'NONE', #9825, .T. ) ;
#12794=CARTESIAN_POINT ( 'NONE',  ( -3.999999999999996447, 1.941961291383473842, -0.3515519931180204893 ) ) ;
#12805=PRODUCT_DEFINITION_SHAPE ( 'NONE', 'NONE',  #11881 ) ;
#12806=DIRECTION ( 'NONE',  ( -1.000000000000000000, -1.665334536937734318E-16, 0.000000000000000000 ) ) ;
#12817=EDGE_CURVE ( 'NONE', #10589, #12258, #8050, .T. ) ;
#12838=VERTEX_POINT ( 'NONE', #9155 ) ;
#12845=CARTESIAN_POINT ( 'NONE',  ( 3.540000644887140613, 2.810673041920858317, -3.302142222888913015 ) ) ;
#12848=CARTESIAN_POINT ( 'NONE',  ( 3.200000000000000178, 5.329070518200750211E-16, 1.599999999999990319 ) ) ;
#12850=CIRCLE ( 'NONE', #4891, 4.000000000000000000 ) ;
#12857=ORIENTED_EDGE ( 'NONE', *, *, #14294, .F. ) ;
#12862=ORIENTED_EDGE ( 'NONE', *, *, #10171, .F. ) ;
#12884=CARTESIAN_POINT ( 'NONE',  ( 2.449848172108562760, 3.432307619358744066, -3.203702292528890272 ) ) ;
#12890=CIRCLE ( 'NONE', #7731, 2.100000000000000977 ) ;
#12922=ORIENTED_EDGE ( 'NONE', *, *, #2745, .T. ) ;
#12925=EDGE_LOOP ( 'NONE', ( #12225, #6172, #11355, #4142, #2159, #8432, #8092 ) ) ;
#12929=DIRECTION ( 'NONE',  ( 1.000000000000000000, 1.665334536937734071E-16, 0.000000000000000000 ) ) ;
#12932=CIRCLE ( 'NONE', #77, 3.000000000000001332 ) ;
#12936=EDGE_CURVE ( 'NONE', #8895, #13013, #3366, .T. ) ;
#12939=DIRECTION ( 'NONE',  ( 1.000000000000000000, 1.665334536937734071E-16, 0.000000000000000000 ) ) ;
#12956=CONICAL_SURFACE ( 'NONE', #315, 2.500000000000002220, 0.9599310885968781459 ) ;
#12972=CARTESIAN_POINT ( 'NONE',  ( 0.6920835326022568568, 4.454600218803893341, -3.297382984111599580 ) ) ;
#12982=ORIENTED_EDGE ( 'NONE', *, *, #11110, .F. ) ;
#12986=ORIENTED_EDGE ( 'NONE', *, *, #11110, .T. ) ;
#12994=DIRECTION ( 'NONE',  ( 1.000000000000000000, 1.665334536937734071E-16, 0.000000000000000000 ) ) ;
#13002=VERTEX_POINT ( 'NONE', #9742 ) ;
#13004=CARTESIAN_POINT ( 'NONE',  ( -0.1404055950190682134, -4.699865361597010960, -3.386887224136959862 ) ) ;
#13009=CARTESIAN_POINT ( 'NONE',  ( 0.000000000000000000, 0.000000000000000000, -25.03750572909319061 ) ) ;
#13013=VERTEX_POINT ( 'NONE', #12308 ) ;
#13016=ORIENTED_EDGE ( 'NONE', *, *, #1174, .T. ) ;
#13029=ORIENTED_EDGE ( 'NONE', *, *, #8491, .F. ) ;
#13040=EDGE_LOOP ( 'NONE', ( #1479, #14141, #10173, #12986 ) ) ;
#13044=VECTOR ( 'NONE', #6094, 1000.000000000000000 ) ;
#13049=EDGE_CURVE ( 'NONE', #8895, #7559, #11985, .T. ) ;
#13051=CIRCLE ( 'NONE', #4657, 4.000000000000000888 ) ;
#13098=CIRCLE ( 'NONE', #7920, 2.540000000000002700 ) ;
#13110=CARTESIAN_POINT ( 'NONE',  ( 4.000000000001417533, -1.677829075513190160, -3.235264651232573119 ) ) ;
#13142=( GEOMETRIC_REPRESENTATION_CONTEXT ( 3 ) GLOBAL_UNCERTAINTY_ASSIGNED_CONTEXT ( ( #14088 ) ) GLOBAL_UNIT_ASSIGNED_CONTEXT ( ( #12155, #6504, #14149 ) ) REPRESENTATION_CONTEXT ( 'NONE', 'WORKASPACE' ) );
#13144=CARTESIAN_POINT ( 'NONE',  ( 0.6666666666666671848, 4.233901974057268092, -3.000726591567076440 ) ) ;
#13148=FACE_OUTER_BOUND ( 'NONE', #4581, .T. ) ;
#13162=CARTESIAN_POINT ( 'NONE',  ( 0.000000000000000000, 0.000000000000000000, 1.599999999999990319 ) ) ;
#13166=CARTESIAN_POINT ( 'NONE',  ( -4.000000000000000000, -2.309401076758511806, -4.699999999999981526 ) ) ;
#13173=CIRCLE ( 'NONE', #2641, 5.384454397937120440 ) ;
#13183=CARTESIAN_POINT ( 'NONE',  ( 4.204114824917655646, -1.660420935435633627, -3.302147294767053154 ) ) ;
#13216=CARTESIAN_POINT ( 'NONE',  ( 4.236525418537980592, -2.416953631397936064, -3.451298686683613060 ) ) ;
#13227=EDGE_CURVE ( 'NONE', #14186, #3878, #2882, .T. ) ;
#13228=DIRECTION ( 'NONE',  ( -1.000000000000000000, -1.665334536937734071E-16, 0.000000000000000000 ) ) ;
#13247=ORIENTED_EDGE ( 'NONE', *, *, #10393, .F. ) ;
#13248=EDGE_CURVE ( 'NONE', #6553, #13013, #12451, .T. ) ;
#13263=DIRECTION ( 'NONE',  ( 1.000000000000000000, 1.665334536937734071E-16, 0.000000000000000000 ) ) ;
#13270=CARTESIAN_POINT ( 'NONE',  ( -0.5636734750058277621, -4.293365120987121308, -3.231543764079341408 ) ) ;
#13280=CIRCLE ( 'NONE', #10223, 3.200000000000000622 ) ;
#13285=LINE ( 'NONE', #4444, #2282 ) ;
#13287=CONICAL_SURFACE ( 'NONE', #5771, 4.000000000000000000, 0.8911886515913775009 ) ;
#13311=DIRECTION ( 'NONE',  ( 1.000000000000000000, 1.665334536937734071E-16, 0.000000000000000000 ) ) ;
#13333=ADVANCED_FACE ( 'NONE', ( #14208 ), #11934, .F. ) ;
#13355=B_SPLINE_CURVE_WITH_KNOTS ( 'NONE', 3,
 ( #11036, #1156, #6563, #863, #1012, #5609 ),
 .UNSPECIFIED., .F., .F.,
 ( 4, 2, 4 ),
 ( 0.000000000000000000, 0.0002095117440854733380, 0.0004190234881709466760 ),
 .UNSPECIFIED. ) ;
#13364=VERTEX_POINT ( 'NONE', #2796 ) ;
#13401=CARTESIAN_POINT ( 'NONE',  ( 3.999999999999998224, 1.658584703716829312, -3.231554742509630707 ) ) ;
#13404=AXIS2_PLACEMENT_3D ( 'NONE', #13439, #12393, #12257 ) ;
#13405=CARTESIAN_POINT ( 'NONE',  ( 0.000000000000000000, 0.000000000000000000, 0.000000000000000000 ) ) ;
#13407=ORIENTED_EDGE ( 'NONE', *, *, #12122, .T. ) ;
#13421=CYLINDRICAL_SURFACE ( 'NONE', #6570, 2.100000000000000977 ) ;
#13422=ORIENTED_EDGE ( 'NONE', *, *, #4661, .T. ) ;
#13424=EDGE_CURVE ( 'NONE', #11445, #6344, #2626, .T. ) ;
#13432=DIRECTION ( 'NONE',  ( -4.406877377903809255E-17, 1.000000000000000000, 0.000000000000000000 ) ) ;
#13439=CARTESIAN_POINT ( 'NONE',  ( 0.000000000000000000, 0.000000000000000000, 0.000000000000000000 ) ) ;
#13463=DIRECTION ( 'NONE',  ( 1.000000000000000000, 1.665334536937734071E-16, 0.000000000000000000 ) ) ;
#13469=B_SPLINE_CURVE_WITH_KNOTS ( 'NONE', 3,
 ( #7276, #11753, #8146, #1731, #639 ),
 .UNSPECIFIED., .F., .F.,
 ( 4, 1, 4 ),
 ( 0.000000000000000000, 0.002309401076758505790, 0.004618802153517011580 ),
 .UNSPECIFIED. ) ;
#13485=ORIENTED_EDGE ( 'NONE', *, *, #13807, .T. ) ;
#13503=FACE_OUTER_BOUND ( 'NONE', #7001, .T. ) ;
#13525=DIRECTION ( 'NONE',  ( -1.000000000000000000, -1.665334536937734071E-16, 0.000000000000000000 ) ) ;
#13533=EDGE_CURVE ( 'NONE', #6911, #8895, #3822, .T. ) ;
#13542=EDGE_LOOP ( 'NONE', ( #8410, #3857 ) ) ;
#13543=CARTESIAN_POINT ( 'NONE',  ( -2.807096675500548866, 3.225959780909076535, -3.202509183706246709 ) ) ;
#13547=DIRECTION ( 'NONE',  ( 1.000000000000000000, 1.665334536937734071E-16, 0.000000000000000000 ) ) ;
#13550=CARTESIAN_POINT ( 'NONE',  ( 3.355112389629170355, -2.681727112203175167, -0.2256878752776822483 ) ) ;
#13564=AXIS2_PLACEMENT_3D ( 'NONE', #10677, #2939, #664 ) ;
#13573=AXIS2_PLACEMENT_3D ( 'NONE', #5954, #11318, #11380 ) ;
#13585=CARTESIAN_POINT ( 'NONE',  ( -2.085819415614008699E-16, -4.647091401871169758, -3.272172305156503480 ) ) ;
#13588=VERTEX_POINT ( 'NONE', #6096 ) ;
#13611=CIRCLE ( 'NONE', #740, 2.100000000000000977 ) ;
#13615=CARTESIAN_POINT ( 'NONE',  ( -3.999999999999990674, -1.680125368658683671, -3.016613018637997357 ) ) ;
#13636=EDGE_CURVE ( 'NONE', #698, #7122, #13469, .T. ) ;
#13639=ORIENTED_EDGE ( 'NONE', *, *, #12141, .F. ) ;
#13669=CARTESIAN_POINT ( 'NONE',  ( 4.140405595019061913, 2.228337868678513800, -3.386887224136951868 ) ) ;
#13680=CARTESIAN_POINT ( 'NONE',  ( 4.000000000000003553, 2.309401076758511806, -0.5000000000000004441 ) ) ;
#13701=CARTESIAN_POINT ( 'NONE',  ( 0.000000000000000000, 0.000000000000000000, 2.400000000000013234 ) ) ;
#13711=VERTEX_POINT ( 'NONE', #11973 ) ;
#13718=ADVANCED_FACE ( 'NONE', ( #9624 ), #10864, .F. ) ;
#13723=DIRECTION ( 'NONE',  ( 0.000000000000000000, 0.000000000000000000, 1.000000000000000000 ) ) ;
#13738=AXIS2_PLACEMENT_3D ( 'NONE', #12848, #11827, #1947 ) ;
#13754=CARTESIAN_POINT ( 'NONE',  ( 0.000000000000000000, 4.618802153517016507, -3.133295621305376422 ) ) ;
#13758=CARTESIAN_POINT ( 'NONE',  ( -0.5276476219777461729, 4.314164656930889130, -3.020318136128642195 ) ) ;
#13759=ORIENTED_EDGE ( 'NONE', *, *, #5681, .T. ) ;
#13765=LINE ( 'NONE', #3734, #1619 ) ;
#13774=ADVANCED_FACE ( 'NONE', ( #13503 ), #2296, .T. ) ;
#13784=CARTESIAN_POINT ( 'NONE',  ( -4.211140560182201398, -2.431303136016548017, -3.445885042887453231 ) ) ;
#13802=ADVANCED_BREP_SHAPE_REPRESENTATION ( '', ( #11581, #11025 ), #11250 ) ;
#13807=EDGE_CURVE ( 'NONE', #14315, #11970, #4369, .T. ) ;
#13824=ADVANCED_FACE ( 'NONE', ( #12179 ), #6839, .T. ) ;
#13850=DIRECTION ( 'NONE',  ( 0.000000000000000000, 0.000000000000000000, 1.000000000000000000 ) ) ;
#13870=CARTESIAN_POINT ( 'NONE',  ( -0.6937372685066646172, 4.453844082567730567, -3.310536846335873751 ) ) ;
#13877=ORIENTED_EDGE ( 'NONE', *, *, #834, .F. ) ;
#13880=CARTESIAN_POINT ( 'NONE',  ( 0.000000000000000000, 0.000000000000000000, -4.674599999999973221 ) ) ;
#13888=EDGE_LOOP ( 'NONE', ( #10581, #5774, #9121, #12862, #7141 ) ) ;
#13900=CARTESIAN_POINT ( 'NONE',  ( -3.999999999999990674, -2.472261030551099914, -3.387027369136278665 ) ) ;
#13910=EDGE_CURVE ( 'NONE', #7536, #13002, #13173, .T. ) ;
#13922=EDGE_CURVE ( 'NONE', #2748, #12258, #6604, .T. ) ;
#13947=DIRECTION ( 'NONE',  ( -1.000000000000000000, -1.665334536937734071E-16, 0.000000000000000000 ) ) ;
#13957=DIRECTION ( 'NONE',  ( 1.000000000000000000, 1.665334536937734071E-16, 0.000000000000000000 ) ) ;
#13967=AXIS2_PLACEMENT_3D ( 'NONE', #1412, #13723, #3850 ) ;
#13974=DIRECTION ( 'NONE',  ( 0.000000000000000000, 0.000000000000000000, 1.000000000000000000 ) ) ;
#13978=CARTESIAN_POINT ( 'NONE',  ( -1.828356344711641102, -3.563200125723192446, -1.069379095908553863E-14 ) ) ;
#14009=CARTESIAN_POINT ( 'NONE',  ( 4.000000000000003553, -2.309401076758511806, -4.699999999999981526 ) ) ;
#14017=CARTESIAN_POINT ( 'NONE',  ( -3.000000000000000000, -1.322063213371142838E-16, 1.599999999999990319 ) ) ;
#14025=ADVANCED_FACE ( 'NONE', ( #1927 ), #2197, .T. ) ;
#14038=EDGE_LOOP ( 'NONE', ( #4833, #13247, #657 ) ) ;
#14088=UNCERTAINTY_MEASURE_WITH_UNIT (LENGTH_MEASURE( 1.000000000000000082E-05 ), #12155, 'distance_accuracy_value', 'NONE');
#14090=TOROIDAL_SURFACE ( 'NONE', #7760, 5.384454397937117776, 0.5155456020628805813 ) ;
#14141=ORIENTED_EDGE ( 'NONE', *, *, #13424, .F. ) ;
#14149=( NAMED_UNIT ( * ) SI_UNIT ( $, .STERADIAN. ) SOLID_ANGLE_UNIT ( ) );
#14156=DIRECTION ( 'NONE',  ( 1.000000000000000000, 1.665334536937734071E-16, 0.000000000000000000 ) ) ;
#14159=ADVANCED_FACE ( 'NONE', ( #7330 ), #12461, .T. ) ;
#14171=CARTESIAN_POINT ( 'NONE',  ( 1.243833333692737186, -3.900674643482489046, -2.923144239647423426 ) ) ;
#14180=ORIENTED_EDGE ( 'NONE', *, *, #4661, .F. ) ;
#14186=VERTEX_POINT ( 'NONE', #3397 ) ;
#14189=DIRECTION ( 'NONE',  ( 0.000000000000000000, 0.000000000000000000, 1.000000000000000000 ) ) ;
#14208=FACE_OUTER_BOUND ( 'NONE', #9052, .T. ) ;
#14244=CARTESIAN_POINT ( 'NONE',  ( 4.198928548860776822, -0.8158838809860106123, -3.226471437616904137 ) ) ;
#14252=ORIENTED_EDGE ( 'NONE', *, *, #2745, .F. ) ;
#14271=CARTESIAN_POINT ( 'NONE',  ( 3.999999999999998224, 2.512222795755935323, -3.169391084040438233 ) ) ;
#14293=CARTESIAN_POINT ( 'NONE',  ( 0.1756478951291663981, -4.720212513052437941, -3.169390900447843329 ) ) ;
#14294=EDGE_CURVE ( 'NONE', #698, #661, #11588, .T. ) ;
#14307=CARTESIAN_POINT ( 'NONE',  ( -5.384454397937117776, -2.411715596982285058E-16, -4.699999999999981526 ) ) ;
#14314=AXIS2_PLACEMENT_3D ( 'NONE', #4079, #969, #8518 ) ;
#14315=VERTEX_POINT ( 'NONE', #9322 ) ;
#14333=ORIENTED_EDGE ( 'NONE', *, *, #8159, .T. ) ;
#14341=ADVANCED_FACE ( 'NONE', ( #2830 ), #12956, .F. ) ;
#14349=DIRECTION ( 'NONE',  ( 1.000000000000000000, 1.665334536937734071E-16, 0.000000000000000000 ) ) ;
#14353=ADVANCED_FACE ( 'NONE', ( #12764 ), #9925, .F. ) ;
#14362=B_SPLINE_CURVE_WITH_KNOTS ( 'NONE', 3,
 ( #2781, #4027, #1591, #1524, #8170, #9503 ),
 .UNSPECIFIED., .F., .F.,
 ( 4, 2, 4 ),
 ( 0.000000000000000000, 0.0002095117440854733651, 0.0004190234881709467302 ),
 .UNSPECIFIED. ) ;
#14365=DIRECTION ( 'NONE',  ( 0.000000000000000000, 0.000000000000000000, -1.000000000000000000 ) ) ;
#14379=LINE ( 'NONE', #1939, #11734 ) ;
#14381=APPLICATION_CONTEXT ( 'automotive_design' ) ;
#14387=ORIENTED_EDGE ( 'NONE', *, *, #241, .T. ) ;
#14388=ORIENTED_EDGE ( 'NONE', *, *, #3124, .T. ) ;
#14389=CARTESIAN_POINT ( 'NONE',  ( 4.204015924366194312, -1.626724848190931771, -3.310627190413377274 ) ) ;
ENDSEC;
END-ISO-10303-21;
